ISO-10303-21;
HEADER;
/* Generated by software containing ST-Developer
 * from STEP Tools, Inc. (www.steptools.com) 
 */

FILE_DESCRIPTION(
/* description */ ('STEP AP214'),
/* implementation_level */ '2;1');

FILE_NAME(
/* name */ 'hex flange nut gradea_iso_ISO - 4161 - M5 - N.step',
/* time_stamp */ '2026-11-04T19:00:26-08:00',
/* author */ (''),
/* organization */ (''),
/* preprocessor_version */ 'ST-DEVELOPER v20.2',
/* originating_system */ 'Autodesk Translation Framework v15.17.0.0',
/* authorisation */ '');

FILE_SCHEMA (('AUTOMOTIVE_DESIGN { 1 0 10303 214 3 1 1 }'));
ENDSEC;

DATA;
#10=MECHANICAL_DESIGN_GEOMETRIC_PRESENTATION_REPRESENTATION('',(#277),#5689);
#199=(
BOUNDED_SURFACE()
B_SPLINE_SURFACE(3,2,((#5358,#5359,#5360),(#5361,#5362,#5363),(#5364,#5365,
#5366),(#5367,#5368,#5369),(#5370,#5371,#5372),(#5373,#5374,#5375)),
 .UNSPECIFIED.,.F.,.F.,.F.)
B_SPLINE_SURFACE_WITH_KNOTS((4,2,4),(3,3),(0.0203285324751813,0.0227886329536482,
0.0252487334321152),(0.,1.),.UNSPECIFIED.)
GEOMETRIC_REPRESENTATION_ITEM()
RATIONAL_B_SPLINE_SURFACE(((1.,0.804778161589684,1.),(1.,0.812376758628819,
1.),(1.,0.819066241556581,1.),(1.,0.81923610156676,1.),(1.,0.812613580710497,
1.),(1.,0.804771233831858,1.)))
REPRESENTATION_ITEM('')
SURFACE()
);
#200=(
BOUNDED_SURFACE()
B_SPLINE_SURFACE(3,2,((#5429,#5430,#5431),(#5432,#5433,#5434),(#5435,#5436,
#5437),(#5438,#5439,#5440),(#5441,#5442,#5443),(#5444,#5445,#5446)),
 .UNSPECIFIED.,.F.,.F.,.F.)
B_SPLINE_SURFACE_WITH_KNOTS((4,2,4),(3,3),(0.0203285324751813,0.0227886329536482,
0.0252487334321152),(0.,1.),.UNSPECIFIED.)
GEOMETRIC_REPRESENTATION_ITEM()
RATIONAL_B_SPLINE_SURFACE(((1.,0.804778161589684,1.),(1.,0.812376758628925,
1.),(1.,0.819066241556439,1.),(1.,0.819236101566903,1.),(1.,0.81261358071039,
1.),(1.,0.804771233831859,1.)))
REPRESENTATION_ITEM('')
SURFACE()
);
#201=(
BOUNDED_SURFACE()
B_SPLINE_SURFACE(3,2,((#5472,#5473,#5474),(#5475,#5476,#5477),(#5478,#5479,
#5480),(#5481,#5482,#5483),(#5484,#5485,#5486),(#5487,#5488,#5489)),
 .UNSPECIFIED.,.F.,.F.,.F.)
B_SPLINE_SURFACE_WITH_KNOTS((4,2,4),(3,3),(0.0202775271026916,0.022737815950911,
0.0251981047991304),(0.,1.),.UNSPECIFIED.)
GEOMETRIC_REPRESENTATION_ITEM()
RATIONAL_B_SPLINE_SURFACE(((1.,0.804778143171281,1.),(1.,0.812377324708393,
1.),(1.,0.819067019215491,1.),(1.,0.819235355291218,1.),(1.,0.812613209822683,
1.),(1.,0.804771246585639,1.)))
REPRESENTATION_ITEM('')
SURFACE()
);
#202=(
BOUNDED_SURFACE()
B_SPLINE_SURFACE(3,2,((#5518,#5519,#5520),(#5521,#5522,#5523),(#5524,#5525,
#5526),(#5527,#5528,#5529),(#5530,#5531,#5532),(#5533,#5534,#5535)),
 .UNSPECIFIED.,.F.,.F.,.F.)
B_SPLINE_SURFACE_WITH_KNOTS((4,2,4),(3,3),(0.0202706586107177,0.0227307226783692,
0.0251907867460207),(0.,1.),.UNSPECIFIED.)
GEOMETRIC_REPRESENTATION_ITEM()
RATIONAL_B_SPLINE_SURFACE(((1.,0.80477817083373,1.),(1.,0.812376519070531,
1.),(1.,0.819065627716398,1.),(1.,0.819236690351216,1.),(1.,0.812613845430289,
1.),(1.,0.804771224603142,1.)))
REPRESENTATION_ITEM('')
SURFACE()
);
#203=(
BOUNDED_SURFACE()
B_SPLINE_SURFACE(3,2,((#5561,#5562,#5563),(#5564,#5565,#5566),(#5567,#5568,
#5569),(#5570,#5571,#5572),(#5573,#5574,#5575),(#5576,#5577,#5578)),
 .UNSPECIFIED.,.F.,.F.,.F.)
B_SPLINE_SURFACE_WITH_KNOTS((4,2,4),(3,3),(0.0203285324751813,0.0227886329536482,
0.0252487334321152),(0.,1.),.UNSPECIFIED.)
GEOMETRIC_REPRESENTATION_ITEM()
RATIONAL_B_SPLINE_SURFACE(((1.,0.804778161589684,1.),(1.,0.812376758628997,
1.),(1.,0.819066241556344,1.),(1.,0.819236101566998,1.),(1.,0.812613580710318,
1.),(1.,0.804771233831859,1.)))
REPRESENTATION_ITEM('')
SURFACE()
);
#204=(
BOUNDED_SURFACE()
B_SPLINE_SURFACE(3,2,((#5607,#5608,#5609),(#5610,#5611,#5612),(#5613,#5614,
#5615),(#5616,#5617,#5618),(#5619,#5620,#5621),(#5622,#5623,#5624)),
 .UNSPECIFIED.,.F.,.F.,.F.)
B_SPLINE_SURFACE_WITH_KNOTS((4,2,4),(3,3),(0.0203285324751813,0.0227886329536482,
0.0252487334321152),(0.,1.),.UNSPECIFIED.)
GEOMETRIC_REPRESENTATION_ITEM()
RATIONAL_B_SPLINE_SURFACE(((1.,0.804778161589684,1.),(1.,0.812376758629104,
1.),(1.,0.819066241556201,1.),(1.,0.81923610156714,1.),(1.,0.812613580710212,
1.),(1.,0.804771233831859,1.)))
REPRESENTATION_ITEM('')
SURFACE()
);
#205=(
BOUNDED_CURVE()
B_SPLINE_CURVE(2,(#5146,#5147,#5148),.UNSPECIFIED.,.F.,.F.)
B_SPLINE_CURVE_WITH_KNOTS((3,3),(0.56122233924649,0.967776243738921),
 .UNSPECIFIED.)
CURVE()
GEOMETRIC_REPRESENTATION_ITEM()
RATIONAL_B_SPLINE_CURVE((1.56483201089635,1.68587218817573,1.68587218817573))
REPRESENTATION_ITEM('')
);
#206=(
BOUNDED_CURVE()
B_SPLINE_CURVE(2,(#5149,#5150,#5151),.UNSPECIFIED.,.F.,.F.)
B_SPLINE_CURVE_WITH_KNOTS((3,3),(0.967776243738921,1.37433014823136),
 .UNSPECIFIED.)
CURVE()
GEOMETRIC_REPRESENTATION_ITEM()
RATIONAL_B_SPLINE_CURVE((1.68587218817573,1.68587218817573,1.56483201089635))
REPRESENTATION_ITEM('')
);
#207=(
BOUNDED_CURVE()
B_SPLINE_CURVE(2,(#5185,#5186,#5187),.UNSPECIFIED.,.F.,.F.)
B_SPLINE_CURVE_WITH_KNOTS((3,3),(0.561222339246465,0.967776243738892),
 .UNSPECIFIED.)
CURVE()
GEOMETRIC_REPRESENTATION_ITEM()
RATIONAL_B_SPLINE_CURVE((1.56483201089633,1.6858721881757,1.6858721881757))
REPRESENTATION_ITEM('')
);
#208=(
BOUNDED_CURVE()
B_SPLINE_CURVE(2,(#5188,#5189,#5190),.UNSPECIFIED.,.F.,.F.)
B_SPLINE_CURVE_WITH_KNOTS((3,3),(0.967776243738892,1.37433014823131),
 .UNSPECIFIED.)
CURVE()
GEOMETRIC_REPRESENTATION_ITEM()
RATIONAL_B_SPLINE_CURVE((1.6858721881757,1.6858721881757,1.56483201089633))
REPRESENTATION_ITEM('')
);
#209=(
BOUNDED_CURVE()
B_SPLINE_CURVE(2,(#5224,#5225,#5226),.UNSPECIFIED.,.F.,.F.)
B_SPLINE_CURVE_WITH_KNOTS((3,3),(0.967776300881118,1.37433022008006),
 .UNSPECIFIED.)
CURVE()
GEOMETRIC_REPRESENTATION_ITEM()
RATIONAL_B_SPLINE_CURVE((1.68587224106752,1.68587224106752,1.56483205999068))
REPRESENTATION_ITEM('')
);
#210=(
BOUNDED_CURVE()
B_SPLINE_CURVE(2,(#5227,#5228,#5229),.UNSPECIFIED.,.F.,.F.)
B_SPLINE_CURVE_WITH_KNOTS((3,3),(0.561222381682178,0.967776300881118),
 .UNSPECIFIED.)
CURVE()
GEOMETRIC_REPRESENTATION_ITEM()
RATIONAL_B_SPLINE_CURVE((1.56483205999068,1.68587224106752,1.68587224106752))
REPRESENTATION_ITEM('')
);
#211=(
BOUNDED_CURVE()
B_SPLINE_CURVE(2,(#5263,#5264,#5265),.UNSPECIFIED.,.F.,.F.)
B_SPLINE_CURVE_WITH_KNOTS((3,3),(0.561222339246487,0.967776243738916),
 .UNSPECIFIED.)
CURVE()
GEOMETRIC_REPRESENTATION_ITEM()
RATIONAL_B_SPLINE_CURVE((1.56483201089635,1.68587218817572,1.68587218817572))
REPRESENTATION_ITEM('')
);
#212=(
BOUNDED_CURVE()
B_SPLINE_CURVE(2,(#5266,#5267,#5268),.UNSPECIFIED.,.F.,.F.)
B_SPLINE_CURVE_WITH_KNOTS((3,3),(0.967776243738916,1.37433014823135),
 .UNSPECIFIED.)
CURVE()
GEOMETRIC_REPRESENTATION_ITEM()
RATIONAL_B_SPLINE_CURVE((1.68587218817572,1.68587218817572,1.56483201089634))
REPRESENTATION_ITEM('')
);
#213=(
BOUNDED_CURVE()
B_SPLINE_CURVE(2,(#5302,#5303,#5304),.UNSPECIFIED.,.F.,.F.)
B_SPLINE_CURVE_WITH_KNOTS((3,3),(0.561222339246469,0.967776243738892),
 .UNSPECIFIED.)
CURVE()
GEOMETRIC_REPRESENTATION_ITEM()
RATIONAL_B_SPLINE_CURVE((1.56483201089633,1.6858721881757,1.6858721881757))
REPRESENTATION_ITEM('')
);
#214=(
BOUNDED_CURVE()
B_SPLINE_CURVE(2,(#5305,#5306,#5307),.UNSPECIFIED.,.F.,.F.)
B_SPLINE_CURVE_WITH_KNOTS((3,3),(0.967776243738892,1.37433014823132),
 .UNSPECIFIED.)
CURVE()
GEOMETRIC_REPRESENTATION_ITEM()
RATIONAL_B_SPLINE_CURVE((1.6858721881757,1.6858721881757,1.56483201089633))
REPRESENTATION_ITEM('')
);
#215=(
BOUNDED_CURVE()
B_SPLINE_CURVE(2,(#5338,#5339,#5340),.UNSPECIFIED.,.F.,.F.)
B_SPLINE_CURVE_WITH_KNOTS((3,3),(0.561222271706646,0.967776152792487),
 .UNSPECIFIED.)
CURVE()
GEOMETRIC_REPRESENTATION_ITEM()
RATIONAL_B_SPLINE_CURVE((1.56483193275875,1.68587210399417,1.68587210399417))
REPRESENTATION_ITEM('')
);
#216=(
BOUNDED_CURVE()
B_SPLINE_CURVE(2,(#5341,#5342,#5343),.UNSPECIFIED.,.F.,.F.)
B_SPLINE_CURVE_WITH_KNOTS((3,3),(0.967776152792487,1.37433003387833),
 .UNSPECIFIED.)
CURVE()
GEOMETRIC_REPRESENTATION_ITEM()
RATIONAL_B_SPLINE_CURVE((1.68587210399417,1.68587210399417,1.56483193275875))
REPRESENTATION_ITEM('')
);
#217=B_SPLINE_CURVE_WITH_KNOTS('',3,(#4935,#4936,#4937,#4938,#4939,#4940),
 .UNSPECIFIED.,.F.,.F.,(4,2,4),(0.00245247880191636,0.003676905084148,0.00490133136637964),
 .UNSPECIFIED.);
#218=B_SPLINE_CURVE_WITH_KNOTS('',3,(#4942,#4943,#4944,#4945,#4946,#4947,
#4948,#4949,#4950,#4951,#4952,#4953,#4954,#4955,#4956,#4957,#4958,#4959,
#4960,#4961,#4962,#4963,#4964,#4965,#4966,#4967,#4968,#4969,#4970,#4971,
#4972),.UNSPECIFIED.,.F.,.F.,(4,3,3,3,3,3,3,3,3,3,4),(5.67844053276549E-16,
0.000695855432601809,0.00134041800879398,0.00193528387732779,0.00245066568318982,
0.00246968402304892,0.00288934416296891,0.0033283699935918,0.00367599852478473,
0.00430462464290023,0.00490133136636978),.UNSPECIFIED.);
#219=B_SPLINE_CURVE_WITH_KNOTS('',3,(#4974,#4975,#4976,#4977,#4978,#4979,
#4980,#4981,#4982,#4983,#4984,#4985,#4986,#4987,#4988,#4989,#4990,#4991,
#4992,#4993,#4994,#4995,#4996,#4997,#4998,#4999,#5000,#5001,#5002,#5003,
#5004),.UNSPECIFIED.,.F.,.F.,(4,3,3,3,3,3,3,3,3,3,4),(8.85358667444219E-15,
0.000695855432697135,0.0013404180089634,0.00193528387756669,0.00245066568318982,
0.00246968402304891,0.00288934416297983,0.00332836999361881,0.00367599852478473,
0.00430462464295834,0.00490133136637964),.UNSPECIFIED.);
#220=B_SPLINE_CURVE_WITH_KNOTS('',3,(#5006,#5007,#5008,#5009,#5010,#5011,
#5012,#5013,#5014,#5015,#5016,#5017,#5018),.UNSPECIFIED.,.F.,.F.,(4,3,3,
3,4),(8.11127826823332E-15,0.000689795867694038,0.00132892982254773,0.00191855771040346,
0.00245247880191638),.UNSPECIFIED.);
#221=B_SPLINE_CURVE_WITH_KNOTS('',3,(#5020,#5021,#5022,#5023,#5024,#5025),
 .UNSPECIFIED.,.F.,.F.,(4,2,4),(0.00245247880191638,0.00367690508414801,
0.00490133136637964),.UNSPECIFIED.);
#222=B_SPLINE_CURVE_WITH_KNOTS('',3,(#5027,#5028,#5029,#5030,#5031,#5032,
#5033,#5034,#5035,#5036,#5037,#5038,#5039,#5040,#5041,#5042,#5043,#5044,
#5045,#5046,#5047,#5048,#5049,#5050,#5051,#5052,#5053,#5054,#5055,#5056,
#5057),.UNSPECIFIED.,.F.,.F.,(4,3,3,3,3,3,3,3,3,3,4),(0.,0.000695855432618481,
0.00134041800882542,0.00193528387737502,0.00245066568318982,0.00246968402304892,
0.00288934416296796,0.003328369993593,0.00367599852478473,0.00430462464290574,
0.00490133136637964),.UNSPECIFIED.);
#223=B_SPLINE_CURVE_WITH_KNOTS('',3,(#5059,#5060,#5061,#5062,#5063,#5064,
#5065,#5066,#5067,#5068,#5069,#5070,#5071,#5072,#5073,#5074,#5075,#5076,
#5077,#5078,#5079,#5080,#5081,#5082,#5083,#5084,#5085,#5086,#5087,#5088,
#5089),.UNSPECIFIED.,.F.,.F.,(4,3,3,3,3,3,3,3,3,3,4),(6.16572492944553E-15,
0.000695855432688955,0.00134041800894962,0.00193528387754702,0.00245066568318982,
0.00246968402304892,0.00288934416297848,0.00332836999361346,0.00367599852478473,
0.00430462464295078,0.00490133136636899),.UNSPECIFIED.);
#224=B_SPLINE_CURVE_WITH_KNOTS('',3,(#5090,#5091,#5092,#5093,#5094,#5095,
#5096,#5097,#5098,#5099,#5100,#5101,#5102),.UNSPECIFIED.,.F.,.F.,(4,3,3,
3,4),(8.40381044765954E-15,0.000702159417341443,0.00135239722254579,0.00195265359751279,
0.00245247880191636),.UNSPECIFIED.);
#225=B_SPLINE_CURVE_WITH_KNOTS('',3,(#5115,#5116,#5117,#5118,#5119,#5120,
#5121,#5122,#5123,#5124,#5125,#5126,#5127,#5128,#5129,#5130,#5131,#5132,
#5133,#5134,#5135,#5136,#5137,#5138,#5139,#5140,#5141,#5142),
 .UNSPECIFIED.,.F.,.F.,(4,3,3,3,3,3,3,3,3,4),(0.,0.000577214184020621,0.0011469145667476,
0.00171936884360262,0.00229182312045765,0.00230940107675851,0.00301372435340778,
0.00346410161513776,0.00418729554271379,0.00461880215351701),
 .UNSPECIFIED.);
#226=B_SPLINE_CURVE_WITH_KNOTS('',3,(#5156,#5157,#5158,#5159,#5160,#5161,
#5162,#5163,#5164,#5165,#5166,#5167,#5168,#5169,#5170,#5171,#5172,#5173,
#5174,#5175,#5176,#5177,#5178,#5179,#5180,#5181,#5182,#5183),
 .UNSPECIFIED.,.F.,.F.,(4,3,3,3,3,3,3,3,3,4),(0.,0.000577214184043689,0.00114691456679992,
0.00171936884362879,0.00229182312045765,0.00230940107675851,0.00301372435351753,
0.00346410161513776,0.00418729554278622,0.00461880215351701),
 .UNSPECIFIED.);
#227=B_SPLINE_CURVE_WITH_KNOTS('',3,(#5195,#5196,#5197,#5198,#5199,#5200,
#5201,#5202,#5203,#5204,#5205,#5206,#5207,#5208,#5209,#5210,#5211,#5212,
#5213,#5214,#5215,#5216,#5217,#5218,#5219,#5220,#5221,#5222),
 .UNSPECIFIED.,.F.,.F.,(4,3,3,3,3,3,3,3,3,4),(0.,0.000577330594159088,0.00114714311141377,
0.00171942025576102,0.00229169740010826,0.00230940107675851,0.00302569686189932,
0.00346410161513776,0.00419584242927921,0.00461880215351701),
 .UNSPECIFIED.);
#228=B_SPLINE_CURVE_WITH_KNOTS('',3,(#5234,#5235,#5236,#5237,#5238,#5239,
#5240,#5241,#5242,#5243,#5244,#5245,#5246,#5247,#5248,#5249,#5250,#5251,
#5252,#5253,#5254,#5255,#5256,#5257,#5258,#5259,#5260,#5261),
 .UNSPECIFIED.,.F.,.F.,(4,3,3,3,3,3,3,3,3,4),(5.64027445225002E-20,0.000577214184015937,
0.00114691456673884,0.00171936884359825,0.00229182312045766,0.00230940107675851,
0.00301372435339581,0.00346410161513776,0.00418729554270106,0.00461880215351701),
 .UNSPECIFIED.);
#229=B_SPLINE_CURVE_WITH_KNOTS('',3,(#5273,#5274,#5275,#5276,#5277,#5278,
#5279,#5280,#5281,#5282,#5283,#5284,#5285,#5286,#5287,#5288,#5289,#5290,
#5291,#5292,#5293,#5294,#5295,#5296,#5297,#5298,#5299,#5300),
 .UNSPECIFIED.,.F.,.F.,(4,3,3,3,3,3,3,3,3,4),(0.,0.000577214184046313,0.00114691456680682,
0.00171936884363224,0.00229182312045766,0.00230940107675851,0.00301372435353412,
0.00346410161513776,0.00418729554279921,0.00461880215351701),
 .UNSPECIFIED.);
#230=B_SPLINE_CURVE_WITH_KNOTS('',3,(#5309,#5310,#5311,#5312,#5313,#5314,
#5315,#5316,#5317,#5318,#5319,#5320,#5321,#5322,#5323,#5324,#5325,#5326,
#5327,#5328,#5329,#5330,#5331,#5332,#5333,#5334,#5335,#5336),
 .UNSPECIFIED.,.F.,.F.,(4,3,3,3,3,3,3,3,3,4),(0.,0.000577241406570222,0.00114696434019859,
0.00171947309771276,0.00229198185522694,0.00230940107675851,0.00300249253020181,
0.00346410161513776,0.00417905459555678,0.00461880215351701),
 .UNSPECIFIED.);
#231=B_SPLINE_CURVE_WITH_KNOTS('',3,(#5376,#5377,#5378,#5379,#5380,#5381,
#5382,#5383,#5384,#5385,#5386,#5387,#5388,#5389,#5390,#5391,#5392,#5393,
#5394,#5395,#5396,#5397,#5398,#5399,#5400,#5401,#5402,#5403),
 .UNSPECIFIED.,.F.,.F.,(4,3,3,3,3,3,3,3,3,4),(-3.64011549240941E-6,7.47064143895679E-5,
0.000141223222716573,0.000200676503540031,0.000206654603400653,0.000259836747040681,
0.000308997427335436,0.000355388984124418,0.000399064790660936,0.000416939475533297),
 .UNSPECIFIED.);
#232=B_SPLINE_CURVE_WITH_KNOTS('',3,(#5404,#5405,#5406,#5407,#5408,#5409,
#5410,#5411,#5412,#5413,#5414,#5415,#5416,#5417,#5418,#5419,#5420,#5421,
#5422,#5423,#5424,#5425,#5426,#5427,#5428),.UNSPECIFIED.,.F.,.F.,(4,3,3,
3,3,3,3,3,4),(1.01092065026796E-8,4.32951812984497E-5,8.98778625374107E-5,
0.000138990149037295,0.00019384384370113,0.000209511744085474,0.000269284051462139,
0.000350197458189693,0.000419023488170948),.UNSPECIFIED.);
#233=B_SPLINE_CURVE_WITH_KNOTS('',3,(#5447,#5448,#5449,#5450,#5451,#5452,
#5453,#5454,#5455,#5456,#5457,#5458,#5459,#5460,#5461,#5462,#5463,#5464,
#5465,#5466,#5467,#5468,#5469,#5470,#5471),.UNSPECIFIED.,.F.,.F.,(4,3,3,
3,3,3,3,3,4),(1.01015226993228E-8,4.32951932790925E-5,8.98778959717681E-5,
0.000138990207648567,0.000193843941248458,0.000209511744085473,0.000269284041837185,
0.000350197471127522,0.000419023488170945),.UNSPECIFIED.);
#234=B_SPLINE_CURVE_WITH_KNOTS('',3,(#5490,#5491,#5492,#5493,#5494,#5495,
#5496,#5497,#5498,#5499,#5500,#5501,#5502,#5503,#5504,#5505,#5506,#5507,
#5508,#5509,#5510,#5511,#5512,#5513,#5514,#5515,#5516,#5517),
 .UNSPECIFIED.,.F.,.F.,(4,3,3,3,3,3,3,3,3,4),(-3.6401154924107E-6,7.47064416297961E-5,
0.000141223236270614,0.000200676508381646,0.000206654603400652,0.000259836793512798,
0.00030899750605435,0.000355389089154961,0.000399064922535254,0.000416939183220073),
 .UNSPECIFIED.);
#235=B_SPLINE_CURVE_WITH_KNOTS('',3,(#5536,#5537,#5538,#5539,#5540,#5541,
#5542,#5543,#5544,#5545,#5546,#5547,#5548,#5549,#5550,#5551,#5552,#5553,
#5554,#5555,#5556,#5557,#5558,#5559,#5560),.UNSPECIFIED.,.F.,.F.,(4,3,3,
3,3,3,3,3,4),(1.04031327899438E-8,4.32954865334447E-5,8.98781822906502E-5,
0.000138990488526855,0.000193844203201864,0.000209511744085473,0.000269284051462561,
0.000350197458172102,0.000419023488170946),.UNSPECIFIED.);
#236=B_SPLINE_CURVE_WITH_KNOTS('',3,(#5579,#5580,#5581,#5582,#5583,#5584,
#5585,#5586,#5587,#5588,#5589,#5590,#5591,#5592,#5593,#5594,#5595,#5596,
#5597,#5598,#5599,#5600,#5601,#5602,#5603,#5604,#5605,#5606),
 .UNSPECIFIED.,.F.,.F.,(4,3,3,3,3,3,3,3,3,4),(-3.64011549240717E-6,7.47064143979229E-5,
0.000141223222725022,0.000200676503549095,0.000206654603400655,0.000259836754628317,
0.000308997440091673,0.000355389000691412,0.0003990648128455,0.00041693917497655),
 .UNSPECIFIED.);
#239=CONICAL_SURFACE('',#3289,2.5,0.959931088596879);
#240=CONICAL_SURFACE('',#3292,2.06,0.959931088596874);
#241=CONICAL_SURFACE('',#3295,5.56078137864557,1.22173047639605);
#242=CONICAL_SURFACE('',#3316,4.,0.891188651591379);
#243=CONICAL_SURFACE('',#3317,4.,0.891188651591379);
#244=CONICAL_SURFACE('',#3318,4.,0.891188651591379);
#245=CONICAL_SURFACE('',#3319,4.,0.891188651591379);
#246=CONICAL_SURFACE('',#3320,4.,0.891188651591379);
#247=CONICAL_SURFACE('',#3321,4.,0.891188651591379);
#256=TOROIDAL_SURFACE('',#3298,5.38445439793712,0.51554560206288);
#263=SHAPE_REPRESENTATION_RELATIONSHIP('SRR','None',#5764,#270);
#270=ADVANCED_BREP_SHAPE_REPRESENTATION('',(#284),#5688);
#277=STYLED_ITEM('',(#5806),#284);
#284=MANIFOLD_SOLID_BREP('Body1',#2967);
#341=FACE_BOUND('',#803,.T.);
#342=FACE_BOUND('',#805,.T.);
#434=PLANE('',#3302);
#435=PLANE('',#3303);
#436=PLANE('',#3304);
#437=PLANE('',#3305);
#438=PLANE('',#3306);
#439=PLANE('',#3307);
#440=PLANE('',#3308);
#441=PLANE('',#3315);
#575=FACE_OUTER_BOUND('',#790,.T.);
#576=FACE_OUTER_BOUND('',#791,.T.);
#577=FACE_OUTER_BOUND('',#792,.T.);
#578=FACE_OUTER_BOUND('',#793,.T.);
#579=FACE_OUTER_BOUND('',#794,.T.);
#580=FACE_OUTER_BOUND('',#795,.T.);
#581=FACE_OUTER_BOUND('',#796,.T.);
#582=FACE_OUTER_BOUND('',#797,.T.);
#583=FACE_OUTER_BOUND('',#798,.T.);
#584=FACE_OUTER_BOUND('',#799,.T.);
#585=FACE_OUTER_BOUND('',#800,.T.);
#586=FACE_OUTER_BOUND('',#801,.T.);
#587=FACE_OUTER_BOUND('',#802,.T.);
#588=FACE_OUTER_BOUND('',#804,.T.);
#589=FACE_OUTER_BOUND('',#806,.T.);
#590=FACE_OUTER_BOUND('',#807,.T.);
#591=FACE_OUTER_BOUND('',#808,.T.);
#592=FACE_OUTER_BOUND('',#809,.T.);
#593=FACE_OUTER_BOUND('',#810,.T.);
#594=FACE_OUTER_BOUND('',#811,.T.);
#595=FACE_OUTER_BOUND('',#812,.T.);
#596=FACE_OUTER_BOUND('',#813,.T.);
#597=FACE_OUTER_BOUND('',#814,.T.);
#598=FACE_OUTER_BOUND('',#815,.T.);
#599=FACE_OUTER_BOUND('',#816,.T.);
#600=FACE_OUTER_BOUND('',#817,.T.);
#790=EDGE_LOOP('',(#2648,#2649,#2650,#2651,#2652));
#791=EDGE_LOOP('',(#2653,#2654,#2655,#2656,#2657,#2658));
#792=EDGE_LOOP('',(#2659,#2660,#2661,#2662));
#793=EDGE_LOOP('',(#2663,#2664,#2665,#2666,#2667,#2668,#2669,#2670,#2671,
#2672,#2673,#2674));
#794=EDGE_LOOP('',(#2675,#2676,#2677,#2678,#2679));
#795=EDGE_LOOP('',(#2680,#2681,#2682,#2683,#2684));
#796=EDGE_LOOP('',(#2685,#2686,#2687,#2688,#2689));
#797=EDGE_LOOP('',(#2690,#2691,#2692,#2693,#2694));
#798=EDGE_LOOP('',(#2695,#2696,#2697,#2698,#2699));
#799=EDGE_LOOP('',(#2700,#2701,#2702,#2703,#2704));
#800=EDGE_LOOP('',(#2705,#2706,#2707,#2708,#2709));
#801=EDGE_LOOP('',(#2710,#2711,#2712,#2713,#2714));
#802=EDGE_LOOP('',(#2715,#2716,#2717,#2718,#2719,#2720));
#803=EDGE_LOOP('',(#2721));
#804=EDGE_LOOP('',(#2722));
#805=EDGE_LOOP('',(#2723));
#806=EDGE_LOOP('',(#2724,#2725,#2726));
#807=EDGE_LOOP('',(#2727,#2728,#2729));
#808=EDGE_LOOP('',(#2730,#2731,#2732));
#809=EDGE_LOOP('',(#2733,#2734,#2735));
#810=EDGE_LOOP('',(#2736,#2737,#2738));
#811=EDGE_LOOP('',(#2739,#2740,#2741));
#812=EDGE_LOOP('',(#2742,#2743,#2744,#2745));
#813=EDGE_LOOP('',(#2746,#2747,#2748,#2749));
#814=EDGE_LOOP('',(#2750,#2751,#2752,#2753,#2754));
#815=EDGE_LOOP('',(#2755,#2756,#2757,#2758,#2759));
#816=EDGE_LOOP('',(#2760,#2761,#2762,#2763));
#817=EDGE_LOOP('',(#2764,#2765,#2766,#2767));
#1038=LINE('',#4912,#1269);
#1039=LINE('',#4920,#1270);
#1040=LINE('',#4926,#1271);
#1041=LINE('',#4933,#1272);
#1042=LINE('',#5109,#1273);
#1043=LINE('',#5113,#1274);
#1044=LINE('',#5144,#1275);
#1045=LINE('',#5155,#1276);
#1046=LINE('',#5194,#1277);
#1047=LINE('',#5233,#1278);
#1048=LINE('',#5272,#1279);
#1269=VECTOR('',#4071,2.5);
#1270=VECTOR('',#4080,2.5);
#1271=VECTOR('',#4087,2.06);
#1272=VECTOR('',#4094,5.56078137864557);
#1273=VECTOR('',#4105,2.1);
#1274=VECTOR('',#4108,1000.);
#1275=VECTOR('',#4109,1000.);
#1276=VECTOR('',#4112,1000.);
#1277=VECTOR('',#4115,1000.);
#1278=VECTOR('',#4118,1000.);
#1279=VECTOR('',#4121,1000.);
#1378=CIRCLE('',#3286,2.5);
#1379=CIRCLE('',#3287,2.5);
#1380=CIRCLE('',#3288,2.5);
#1381=CIRCLE('',#3290,2.1);
#1382=CIRCLE('',#3291,2.1);
#1383=CIRCLE('',#3293,2.1);
#1384=CIRCLE('',#3294,2.5);
#1385=CIRCLE('',#3296,5.56078137864557);
#1386=CIRCLE('',#3297,5.56078137864557);
#1387=CIRCLE('',#3299,0.51554560206288);
#1388=CIRCLE('',#3300,5.38445439793712);
#1389=CIRCLE('',#3309,4.);
#1390=CIRCLE('',#3310,4.);
#1391=CIRCLE('',#3311,4.);
#1392=CIRCLE('',#3312,4.);
#1393=CIRCLE('',#3313,4.);
#1394=CIRCLE('',#3314,4.);
#1598=VERTEX_POINT('',#4909);
#1599=VERTEX_POINT('',#4911);
#1600=VERTEX_POINT('',#4913);
#1601=VERTEX_POINT('',#4917);
#1602=VERTEX_POINT('',#4918);
#1603=VERTEX_POINT('',#4923);
#1604=VERTEX_POINT('',#4925);
#1605=VERTEX_POINT('',#4929);
#1606=VERTEX_POINT('',#4930);
#1607=VERTEX_POINT('',#4932);
#1608=VERTEX_POINT('',#4934);
#1609=VERTEX_POINT('',#4941);
#1610=VERTEX_POINT('',#4973);
#1611=VERTEX_POINT('',#5005);
#1612=VERTEX_POINT('',#5019);
#1613=VERTEX_POINT('',#5026);
#1614=VERTEX_POINT('',#5058);
#1615=VERTEX_POINT('',#5105);
#1616=VERTEX_POINT('',#5111);
#1617=VERTEX_POINT('',#5112);
#1618=VERTEX_POINT('',#5114);
#1619=VERTEX_POINT('',#5143);
#1620=VERTEX_POINT('',#5145);
#1621=VERTEX_POINT('',#5153);
#1622=VERTEX_POINT('',#5154);
#1623=VERTEX_POINT('',#5184);
#1624=VERTEX_POINT('',#5192);
#1625=VERTEX_POINT('',#5193);
#1626=VERTEX_POINT('',#5223);
#1627=VERTEX_POINT('',#5231);
#1628=VERTEX_POINT('',#5232);
#1629=VERTEX_POINT('',#5262);
#1630=VERTEX_POINT('',#5270);
#1631=VERTEX_POINT('',#5271);
#1632=VERTEX_POINT('',#5301);
#1633=VERTEX_POINT('',#5337);
#1952=EDGE_CURVE('',#1598,#1598,#1378,.T.);
#1953=EDGE_CURVE('',#1598,#1599,#1038,.T.);
#1954=EDGE_CURVE('',#1599,#1600,#1379,.T.);
#1955=EDGE_CURVE('',#1600,#1599,#1380,.T.);
#1956=EDGE_CURVE('',#1601,#1602,#1381,.T.);
#1957=EDGE_CURVE('',#1602,#1600,#1039,.T.);
#1958=EDGE_CURVE('',#1602,#1601,#1382,.T.);
#1959=EDGE_CURVE('',#1603,#1603,#1383,.T.);
#1960=EDGE_CURVE('',#1603,#1604,#1040,.T.);
#1961=EDGE_CURVE('',#1604,#1604,#1384,.T.);
#1962=EDGE_CURVE('',#1605,#1606,#1385,.T.);
#1963=EDGE_CURVE('',#1606,#1607,#1041,.T.);
#1964=EDGE_CURVE('',#1607,#1608,#217,.T.);
#1965=EDGE_CURVE('',#1608,#1609,#218,.T.);
#1966=EDGE_CURVE('',#1609,#1610,#219,.T.);
#1967=EDGE_CURVE('',#1610,#1611,#220,.T.);
#1968=EDGE_CURVE('',#1611,#1612,#221,.T.);
#1969=EDGE_CURVE('',#1612,#1613,#222,.T.);
#1970=EDGE_CURVE('',#1613,#1614,#223,.T.);
#1971=EDGE_CURVE('',#1614,#1607,#224,.T.);
#1972=EDGE_CURVE('',#1606,#1605,#1386,.T.);
#1973=EDGE_CURVE('',#1605,#1615,#1387,.T.);
#1974=EDGE_CURVE('',#1615,#1615,#1388,.T.);
#1975=EDGE_CURVE('',#1601,#1603,#1042,.T.);
#1976=EDGE_CURVE('',#1616,#1617,#1043,.T.);
#1977=EDGE_CURVE('',#1616,#1618,#225,.T.);
#1978=EDGE_CURVE('',#1618,#1619,#1044,.T.);
#1979=EDGE_CURVE('',#1619,#1620,#205,.T.);
#1980=EDGE_CURVE('',#1620,#1617,#206,.T.);
#1981=EDGE_CURVE('',#1621,#1622,#1045,.T.);
#1982=EDGE_CURVE('',#1621,#1616,#226,.T.);
#1983=EDGE_CURVE('',#1617,#1623,#207,.T.);
#1984=EDGE_CURVE('',#1623,#1622,#208,.T.);
#1985=EDGE_CURVE('',#1624,#1625,#1046,.T.);
#1986=EDGE_CURVE('',#1624,#1621,#227,.T.);
#1987=EDGE_CURVE('',#1626,#1622,#209,.T.);
#1988=EDGE_CURVE('',#1625,#1626,#210,.T.);
#1989=EDGE_CURVE('',#1627,#1628,#1047,.T.);
#1990=EDGE_CURVE('',#1627,#1624,#228,.T.);
#1991=EDGE_CURVE('',#1625,#1629,#211,.T.);
#1992=EDGE_CURVE('',#1629,#1628,#212,.T.);
#1993=EDGE_CURVE('',#1630,#1631,#1048,.T.);
#1994=EDGE_CURVE('',#1630,#1627,#229,.T.);
#1995=EDGE_CURVE('',#1628,#1632,#213,.T.);
#1996=EDGE_CURVE('',#1632,#1631,#214,.T.);
#1997=EDGE_CURVE('',#1618,#1630,#230,.T.);
#1998=EDGE_CURVE('',#1631,#1633,#215,.T.);
#1999=EDGE_CURVE('',#1633,#1619,#216,.T.);
#2000=EDGE_CURVE('',#1633,#1620,#1389,.T.);
#2001=EDGE_CURVE('',#1632,#1633,#1390,.T.);
#2002=EDGE_CURVE('',#1629,#1632,#1391,.T.);
#2003=EDGE_CURVE('',#1626,#1629,#1392,.T.);
#2004=EDGE_CURVE('',#1626,#1623,#1393,.T.);
#2005=EDGE_CURVE('',#1620,#1623,#1394,.T.);
#2006=EDGE_CURVE('',#1610,#1630,#231,.T.);
#2007=EDGE_CURVE('',#1627,#1609,#232,.T.);
#2008=EDGE_CURVE('',#1624,#1608,#233,.T.);
#2009=EDGE_CURVE('',#1612,#1618,#234,.T.);
#2010=EDGE_CURVE('',#1621,#1614,#235,.T.);
#2011=EDGE_CURVE('',#1613,#1616,#236,.T.);
#2648=ORIENTED_EDGE('',*,*,#1952,.F.);
#2649=ORIENTED_EDGE('',*,*,#1953,.T.);
#2650=ORIENTED_EDGE('',*,*,#1954,.T.);
#2651=ORIENTED_EDGE('',*,*,#1955,.T.);
#2652=ORIENTED_EDGE('',*,*,#1953,.F.);
#2653=ORIENTED_EDGE('',*,*,#1956,.T.);
#2654=ORIENTED_EDGE('',*,*,#1957,.T.);
#2655=ORIENTED_EDGE('',*,*,#1954,.F.);
#2656=ORIENTED_EDGE('',*,*,#1955,.F.);
#2657=ORIENTED_EDGE('',*,*,#1957,.F.);
#2658=ORIENTED_EDGE('',*,*,#1958,.T.);
#2659=ORIENTED_EDGE('',*,*,#1959,.T.);
#2660=ORIENTED_EDGE('',*,*,#1960,.T.);
#2661=ORIENTED_EDGE('',*,*,#1961,.T.);
#2662=ORIENTED_EDGE('',*,*,#1960,.F.);
#2663=ORIENTED_EDGE('',*,*,#1962,.T.);
#2664=ORIENTED_EDGE('',*,*,#1963,.T.);
#2665=ORIENTED_EDGE('',*,*,#1964,.T.);
#2666=ORIENTED_EDGE('',*,*,#1965,.T.);
#2667=ORIENTED_EDGE('',*,*,#1966,.T.);
#2668=ORIENTED_EDGE('',*,*,#1967,.T.);
#2669=ORIENTED_EDGE('',*,*,#1968,.T.);
#2670=ORIENTED_EDGE('',*,*,#1969,.T.);
#2671=ORIENTED_EDGE('',*,*,#1970,.T.);
#2672=ORIENTED_EDGE('',*,*,#1971,.T.);
#2673=ORIENTED_EDGE('',*,*,#1963,.F.);
#2674=ORIENTED_EDGE('',*,*,#1972,.T.);
#2675=ORIENTED_EDGE('',*,*,#1962,.F.);
#2676=ORIENTED_EDGE('',*,*,#1973,.T.);
#2677=ORIENTED_EDGE('',*,*,#1974,.T.);
#2678=ORIENTED_EDGE('',*,*,#1973,.F.);
#2679=ORIENTED_EDGE('',*,*,#1972,.F.);
#2680=ORIENTED_EDGE('',*,*,#1956,.F.);
#2681=ORIENTED_EDGE('',*,*,#1975,.T.);
#2682=ORIENTED_EDGE('',*,*,#1959,.F.);
#2683=ORIENTED_EDGE('',*,*,#1975,.F.);
#2684=ORIENTED_EDGE('',*,*,#1958,.F.);
#2685=ORIENTED_EDGE('',*,*,#1976,.F.);
#2686=ORIENTED_EDGE('',*,*,#1977,.T.);
#2687=ORIENTED_EDGE('',*,*,#1978,.T.);
#2688=ORIENTED_EDGE('',*,*,#1979,.T.);
#2689=ORIENTED_EDGE('',*,*,#1980,.T.);
#2690=ORIENTED_EDGE('',*,*,#1981,.F.);
#2691=ORIENTED_EDGE('',*,*,#1982,.T.);
#2692=ORIENTED_EDGE('',*,*,#1976,.T.);
#2693=ORIENTED_EDGE('',*,*,#1983,.T.);
#2694=ORIENTED_EDGE('',*,*,#1984,.T.);
#2695=ORIENTED_EDGE('',*,*,#1985,.F.);
#2696=ORIENTED_EDGE('',*,*,#1986,.T.);
#2697=ORIENTED_EDGE('',*,*,#1981,.T.);
#2698=ORIENTED_EDGE('',*,*,#1987,.F.);
#2699=ORIENTED_EDGE('',*,*,#1988,.F.);
#2700=ORIENTED_EDGE('',*,*,#1989,.F.);
#2701=ORIENTED_EDGE('',*,*,#1990,.T.);
#2702=ORIENTED_EDGE('',*,*,#1985,.T.);
#2703=ORIENTED_EDGE('',*,*,#1991,.T.);
#2704=ORIENTED_EDGE('',*,*,#1992,.T.);
#2705=ORIENTED_EDGE('',*,*,#1993,.F.);
#2706=ORIENTED_EDGE('',*,*,#1994,.T.);
#2707=ORIENTED_EDGE('',*,*,#1989,.T.);
#2708=ORIENTED_EDGE('',*,*,#1995,.T.);
#2709=ORIENTED_EDGE('',*,*,#1996,.T.);
#2710=ORIENTED_EDGE('',*,*,#1978,.F.);
#2711=ORIENTED_EDGE('',*,*,#1997,.T.);
#2712=ORIENTED_EDGE('',*,*,#1993,.T.);
#2713=ORIENTED_EDGE('',*,*,#1998,.T.);
#2714=ORIENTED_EDGE('',*,*,#1999,.T.);
#2715=ORIENTED_EDGE('',*,*,#2000,.F.);
#2716=ORIENTED_EDGE('',*,*,#2001,.F.);
#2717=ORIENTED_EDGE('',*,*,#2002,.F.);
#2718=ORIENTED_EDGE('',*,*,#2003,.F.);
#2719=ORIENTED_EDGE('',*,*,#2004,.T.);
#2720=ORIENTED_EDGE('',*,*,#2005,.F.);
#2721=ORIENTED_EDGE('',*,*,#1961,.F.);
#2722=ORIENTED_EDGE('',*,*,#1974,.F.);
#2723=ORIENTED_EDGE('',*,*,#1952,.T.);
#2724=ORIENTED_EDGE('',*,*,#2001,.T.);
#2725=ORIENTED_EDGE('',*,*,#1998,.F.);
#2726=ORIENTED_EDGE('',*,*,#1996,.F.);
#2727=ORIENTED_EDGE('',*,*,#2002,.T.);
#2728=ORIENTED_EDGE('',*,*,#1995,.F.);
#2729=ORIENTED_EDGE('',*,*,#1992,.F.);
#2730=ORIENTED_EDGE('',*,*,#1988,.T.);
#2731=ORIENTED_EDGE('',*,*,#2003,.T.);
#2732=ORIENTED_EDGE('',*,*,#1991,.F.);
#2733=ORIENTED_EDGE('',*,*,#2004,.F.);
#2734=ORIENTED_EDGE('',*,*,#1987,.T.);
#2735=ORIENTED_EDGE('',*,*,#1984,.F.);
#2736=ORIENTED_EDGE('',*,*,#2005,.T.);
#2737=ORIENTED_EDGE('',*,*,#1983,.F.);
#2738=ORIENTED_EDGE('',*,*,#1980,.F.);
#2739=ORIENTED_EDGE('',*,*,#1999,.F.);
#2740=ORIENTED_EDGE('',*,*,#2000,.T.);
#2741=ORIENTED_EDGE('',*,*,#1979,.F.);
#2742=ORIENTED_EDGE('',*,*,#2006,.F.);
#2743=ORIENTED_EDGE('',*,*,#1966,.F.);
#2744=ORIENTED_EDGE('',*,*,#2007,.F.);
#2745=ORIENTED_EDGE('',*,*,#1994,.F.);
#2746=ORIENTED_EDGE('',*,*,#2007,.T.);
#2747=ORIENTED_EDGE('',*,*,#1965,.F.);
#2748=ORIENTED_EDGE('',*,*,#2008,.F.);
#2749=ORIENTED_EDGE('',*,*,#1990,.F.);
#2750=ORIENTED_EDGE('',*,*,#2006,.T.);
#2751=ORIENTED_EDGE('',*,*,#1997,.F.);
#2752=ORIENTED_EDGE('',*,*,#2009,.F.);
#2753=ORIENTED_EDGE('',*,*,#1968,.F.);
#2754=ORIENTED_EDGE('',*,*,#1967,.F.);
#2755=ORIENTED_EDGE('',*,*,#2008,.T.);
#2756=ORIENTED_EDGE('',*,*,#1964,.F.);
#2757=ORIENTED_EDGE('',*,*,#1971,.F.);
#2758=ORIENTED_EDGE('',*,*,#2010,.F.);
#2759=ORIENTED_EDGE('',*,*,#1986,.F.);
#2760=ORIENTED_EDGE('',*,*,#2009,.T.);
#2761=ORIENTED_EDGE('',*,*,#1977,.F.);
#2762=ORIENTED_EDGE('',*,*,#2011,.F.);
#2763=ORIENTED_EDGE('',*,*,#1969,.F.);
#2764=ORIENTED_EDGE('',*,*,#2010,.T.);
#2765=ORIENTED_EDGE('',*,*,#1970,.F.);
#2766=ORIENTED_EDGE('',*,*,#2011,.T.);
#2767=ORIENTED_EDGE('',*,*,#1982,.F.);
#2800=CYLINDRICAL_SURFACE('',#3285,2.5);
#2801=CYLINDRICAL_SURFACE('',#3301,2.1);
#2935=ADVANCED_FACE('',(#575),#2800,.F.);
#2936=ADVANCED_FACE('',(#576),#239,.F.);
#2937=ADVANCED_FACE('',(#577),#240,.F.);
#2938=ADVANCED_FACE('',(#578),#241,.T.);
#2939=ADVANCED_FACE('',(#579),#256,.T.);
#2940=ADVANCED_FACE('',(#580),#2801,.F.);
#2941=ADVANCED_FACE('',(#581),#434,.T.);
#2942=ADVANCED_FACE('',(#582),#435,.T.);
#2943=ADVANCED_FACE('',(#583),#436,.F.);
#2944=ADVANCED_FACE('',(#584),#437,.T.);
#2945=ADVANCED_FACE('',(#585),#438,.T.);
#2946=ADVANCED_FACE('',(#586),#439,.T.);
#2947=ADVANCED_FACE('',(#587,#341),#440,.F.);
#2948=ADVANCED_FACE('',(#588,#342),#441,.T.);
#2949=ADVANCED_FACE('',(#589),#242,.T.);
#2950=ADVANCED_FACE('',(#590),#243,.T.);
#2951=ADVANCED_FACE('',(#591),#244,.T.);
#2952=ADVANCED_FACE('',(#592),#245,.T.);
#2953=ADVANCED_FACE('',(#593),#246,.T.);
#2954=ADVANCED_FACE('',(#594),#247,.T.);
#2955=ADVANCED_FACE('',(#595),#199,.F.);
#2956=ADVANCED_FACE('',(#596),#200,.F.);
#2957=ADVANCED_FACE('',(#597),#201,.F.);
#2958=ADVANCED_FACE('',(#598),#202,.F.);
#2959=ADVANCED_FACE('',(#599),#203,.F.);
#2960=ADVANCED_FACE('',(#600),#204,.F.);
#2967=CLOSED_SHELL('',(#2935,#2936,#2937,#2938,#2939,#2940,#2941,#2942,
#2943,#2944,#2945,#2946,#2947,#2948,#2949,#2950,#2951,#2952,#2953,#2954,
#2955,#2956,#2957,#2958,#2959,#2960));
#3284=AXIS2_PLACEMENT_3D('',#4907,#4065,#4066);
#3285=AXIS2_PLACEMENT_3D('',#4908,#4067,#4068);
#3286=AXIS2_PLACEMENT_3D('',#4910,#4069,#4070);
#3287=AXIS2_PLACEMENT_3D('',#4914,#4072,#4073);
#3288=AXIS2_PLACEMENT_3D('',#4915,#4074,#4075);
#3289=AXIS2_PLACEMENT_3D('',#4916,#4076,#4077);
#3290=AXIS2_PLACEMENT_3D('',#4919,#4078,#4079);
#3291=AXIS2_PLACEMENT_3D('',#4921,#4081,#4082);
#3292=AXIS2_PLACEMENT_3D('',#4922,#4083,#4084);
#3293=AXIS2_PLACEMENT_3D('',#4924,#4085,#4086);
#3294=AXIS2_PLACEMENT_3D('',#4927,#4088,#4089);
#3295=AXIS2_PLACEMENT_3D('',#4928,#4090,#4091);
#3296=AXIS2_PLACEMENT_3D('',#4931,#4092,#4093);
#3297=AXIS2_PLACEMENT_3D('',#5103,#4095,#4096);
#3298=AXIS2_PLACEMENT_3D('',#5104,#4097,#4098);
#3299=AXIS2_PLACEMENT_3D('',#5106,#4099,#4100);
#3300=AXIS2_PLACEMENT_3D('',#5107,#4101,#4102);
#3301=AXIS2_PLACEMENT_3D('',#5108,#4103,#4104);
#3302=AXIS2_PLACEMENT_3D('',#5110,#4106,#4107);
#3303=AXIS2_PLACEMENT_3D('',#5152,#4110,#4111);
#3304=AXIS2_PLACEMENT_3D('',#5191,#4113,#4114);
#3305=AXIS2_PLACEMENT_3D('',#5230,#4116,#4117);
#3306=AXIS2_PLACEMENT_3D('',#5269,#4119,#4120);
#3307=AXIS2_PLACEMENT_3D('',#5308,#4122,#4123);
#3308=AXIS2_PLACEMENT_3D('',#5344,#4124,#4125);
#3309=AXIS2_PLACEMENT_3D('',#5345,#4126,#4127);
#3310=AXIS2_PLACEMENT_3D('',#5346,#4128,#4129);
#3311=AXIS2_PLACEMENT_3D('',#5347,#4130,#4131);
#3312=AXIS2_PLACEMENT_3D('',#5348,#4132,#4133);
#3313=AXIS2_PLACEMENT_3D('',#5349,#4134,#4135);
#3314=AXIS2_PLACEMENT_3D('',#5350,#4136,#4137);
#3315=AXIS2_PLACEMENT_3D('',#5351,#4138,#4139);
#3316=AXIS2_PLACEMENT_3D('',#5352,#4140,#4141);
#3317=AXIS2_PLACEMENT_3D('',#5353,#4142,#4143);
#3318=AXIS2_PLACEMENT_3D('',#5354,#4144,#4145);
#3319=AXIS2_PLACEMENT_3D('',#5355,#4146,#4147);
#3320=AXIS2_PLACEMENT_3D('',#5356,#4148,#4149);
#3321=AXIS2_PLACEMENT_3D('',#5357,#4150,#4151);
#4065=DIRECTION('axis',(0.,0.,1.));
#4066=DIRECTION('refdir',(1.,0.,0.));
#4067=DIRECTION('center_axis',(0.,0.,1.));
#4068=DIRECTION('ref_axis',(1.,0.,0.));
#4069=DIRECTION('center_axis',(0.,0.,1.));
#4070=DIRECTION('ref_axis',(-1.,0.,0.));
#4071=DIRECTION('',(0.,0.,1.));
#4072=DIRECTION('center_axis',(0.,0.,1.));
#4073=DIRECTION('ref_axis',(1.,0.,0.));
#4074=DIRECTION('center_axis',(0.,0.,1.));
#4075=DIRECTION('ref_axis',(1.,0.,0.));
#4076=DIRECTION('center_axis',(0.,0.,-1.));
#4077=DIRECTION('ref_axis',(-1.,0.,0.));
#4078=DIRECTION('center_axis',(0.,0.,1.));
#4079=DIRECTION('ref_axis',(-1.,0.,0.));
#4080=DIRECTION('',(0.81915204428899,-1.00317192905352E-16,-0.573576436351048));
#4081=DIRECTION('center_axis',(0.,0.,1.));
#4082=DIRECTION('ref_axis',(-1.,0.,0.));
#4083=DIRECTION('center_axis',(0.,0.,1.));
#4084=DIRECTION('ref_axis',(1.,0.,0.));
#4085=DIRECTION('center_axis',(0.,0.,-1.));
#4086=DIRECTION('ref_axis',(1.,0.,0.));
#4087=DIRECTION('',(-0.819152044288988,-1.00317192905352E-16,0.573576436351052));
#4088=DIRECTION('center_axis',(0.,0.,1.));
#4089=DIRECTION('ref_axis',(1.,0.,0.));
#4090=DIRECTION('center_axis',(0.,0.,-1.));
#4091=DIRECTION('ref_axis',(-1.,0.,0.));
#4092=DIRECTION('center_axis',(0.,0.,1.));
#4093=DIRECTION('ref_axis',(1.,0.,0.));
#4094=DIRECTION('',(-0.939692620785914,1.15079156022786E-16,0.342020143325654));
#4095=DIRECTION('center_axis',(0.,0.,1.));
#4096=DIRECTION('ref_axis',(1.,0.,0.));
#4097=DIRECTION('center_axis',(0.,0.,1.));
#4098=DIRECTION('ref_axis',(1.,0.,0.));
#4099=DIRECTION('center_axis',(1.22464679914735E-16,-1.,0.));
#4100=DIRECTION('ref_axis',(-1.,-1.22464679914735E-16,0.));
#4101=DIRECTION('center_axis',(0.,0.,1.));
#4102=DIRECTION('ref_axis',(1.,0.,0.));
#4103=DIRECTION('center_axis',(0.,0.,1.));
#4104=DIRECTION('ref_axis',(1.,0.,0.));
#4105=DIRECTION('',(0.,0.,1.));
#4106=DIRECTION('center_axis',(-0.500000000000002,0.866025403784438,0.));
#4107=DIRECTION('ref_axis',(-0.866025403784438,-0.500000000000002,0.));
#4108=DIRECTION('',(0.,0.,1.));
#4109=DIRECTION('',(0.,0.,1.));
#4110=DIRECTION('center_axis',(0.500000000000002,0.866025403784437,0.));
#4111=DIRECTION('ref_axis',(-0.866025403784437,0.500000000000002,0.));
#4112=DIRECTION('',(0.,0.,1.));
#4113=DIRECTION('center_axis',(-1.,0.,0.));
#4114=DIRECTION('ref_axis',(0.,0.,1.));
#4115=DIRECTION('',(0.,0.,1.));
#4116=DIRECTION('center_axis',(0.500000000000001,-0.866025403784438,0.));
#4117=DIRECTION('ref_axis',(0.866025403784438,0.500000000000001,0.));
#4118=DIRECTION('',(0.,0.,1.));
#4119=DIRECTION('center_axis',(-0.500000000000002,-0.866025403784438,0.));
#4120=DIRECTION('ref_axis',(0.866025403784437,-0.500000000000002,0.));
#4121=DIRECTION('',(0.,0.,1.));
#4122=DIRECTION('center_axis',(-1.,0.,0.));
#4123=DIRECTION('ref_axis',(0.,0.,1.));
#4124=DIRECTION('center_axis',(0.,0.,-1.));
#4125=DIRECTION('ref_axis',(-1.,0.,0.));
#4126=DIRECTION('center_axis',(0.,0.,-1.));
#4127=DIRECTION('ref_axis',(-1.,0.,0.));
#4128=DIRECTION('center_axis',(0.,0.,-1.));
#4129=DIRECTION('ref_axis',(-1.,0.,0.));
#4130=DIRECTION('center_axis',(0.,0.,-1.));
#4131=DIRECTION('ref_axis',(-1.,0.,0.));
#4132=DIRECTION('center_axis',(0.,0.,-1.));
#4133=DIRECTION('ref_axis',(-1.,0.,0.));
#4134=DIRECTION('center_axis',(0.,0.,1.));
#4135=DIRECTION('ref_axis',(1.,0.,0.));
#4136=DIRECTION('center_axis',(0.,0.,-1.));
#4137=DIRECTION('ref_axis',(-1.,0.,0.));
#4138=DIRECTION('center_axis',(0.,0.,-1.));
#4139=DIRECTION('ref_axis',(-1.,0.,0.));
#4140=DIRECTION('center_axis',(0.,0.,-1.));
#4141=DIRECTION('ref_axis',(-1.,0.,0.));
#4142=DIRECTION('center_axis',(0.,0.,-1.));
#4143=DIRECTION('ref_axis',(-1.,0.,0.));
#4144=DIRECTION('center_axis',(0.,0.,-1.));
#4145=DIRECTION('ref_axis',(-1.,0.,0.));
#4146=DIRECTION('center_axis',(0.,0.,-1.));
#4147=DIRECTION('ref_axis',(-1.,0.,0.));
#4148=DIRECTION('center_axis',(0.,0.,-1.));
#4149=DIRECTION('ref_axis',(-1.,0.,0.));
#4150=DIRECTION('center_axis',(0.,0.,-1.));
#4151=DIRECTION('ref_axis',(-1.,0.,0.));
#4907=CARTESIAN_POINT('',(0.,0.,0.));
#4908=CARTESIAN_POINT('Origin',(0.,0.,-25.0375057290932));
#4909=CARTESIAN_POINT('',(-2.5,-3.06161699786838E-16,-5.));
#4910=CARTESIAN_POINT('Origin',(0.,0.,-5.));
#4911=CARTESIAN_POINT('',(-2.5,-3.06161699786838E-16,-4.9746));
#4912=CARTESIAN_POINT('',(-2.5,-3.06161699786838E-16,-25.0375057290932));
#4913=CARTESIAN_POINT('',(2.5,3.06161699786838E-16,-4.9746));
#4914=CARTESIAN_POINT('Origin',(0.,0.,-4.9746));
#4915=CARTESIAN_POINT('Origin',(0.,0.,-4.9746));
#4916=CARTESIAN_POINT('Origin',(0.,0.,-4.9746));
#4917=CARTESIAN_POINT('',(-2.1,2.57175827820944E-16,-4.69451698471611));
#4918=CARTESIAN_POINT('',(2.1,-2.57175827820944E-16,-4.69451698471611));
#4919=CARTESIAN_POINT('Origin',(0.,0.,-4.69451698471611));
#4920=CARTESIAN_POINT('',(2.5,-3.06161699786838E-16,-4.9746));
#4921=CARTESIAN_POINT('Origin',(0.,0.,-4.69451698471611));
#4922=CARTESIAN_POINT('Origin',(0.,0.,-0.308091316812274));
#4923=CARTESIAN_POINT('',(-2.1,-2.57175827820944E-16,-0.280083015283885));
#4924=CARTESIAN_POINT('Origin',(0.,0.,-0.280083015283884));
#4925=CARTESIAN_POINT('',(-2.5,-3.06161699786838E-16,3.71230823859037E-15));
#4926=CARTESIAN_POINT('',(-2.06,-2.52277240624355E-16,-0.308091316812274));
#4927=CARTESIAN_POINT('Origin',(0.,0.,3.46944695195361E-15));
#4928=CARTESIAN_POINT('Origin',(0.,0.,-4.));
#4929=CARTESIAN_POINT('',(-5.56078137864558,6.80999311611651E-16,-4.));
#4930=CARTESIAN_POINT('',(5.56078137864557,-6.80999311611651E-16,-4.));
#4931=CARTESIAN_POINT('Origin',(0.,0.,-4.));
#4932=CARTESIAN_POINT('',(4.19739386533236,-1.63989485852606E-11,-3.5037678126099));
#4933=CARTESIAN_POINT('',(5.56078137864557,-6.80999311611651E-16,-4.));
#4934=CARTESIAN_POINT('',(4.21114047113378,-2.43130308459281,-3.74588532543563));
#4935=CARTESIAN_POINT('Ctrl Pts',(4.1973939570023,7.7729029084661E-14,-3.50376756074893));
#4936=CARTESIAN_POINT('Ctrl Pts',(4.1973939570023,-0.406987107455746,-3.50376756074893));
#4937=CARTESIAN_POINT('Ctrl Pts',(4.19892854886077,-0.815883880986012,-3.52647143761692));
#4938=CARTESIAN_POINT('Ctrl Pts',(4.20401592436619,-1.62672484819093,-3.61062719041339));
#4939=CARTESIAN_POINT('Ctrl Pts',(4.20749145004057,-2.02981982514649,-3.67167082875957));
#4940=CARTESIAN_POINT('Ctrl Pts',(4.2111405601822,-2.43130313601656,-3.74588504288744));
#4941=CARTESIAN_POINT('',(7.14602004806277E-12,-4.86260614339647,-3.74588539632542));
#4942=CARTESIAN_POINT('Ctrl Pts',(4.21114036026457,-2.4313030205652,-3.74588567721715));
#4943=CARTESIAN_POINT('Ctrl Pts',(4.01254994076142,-2.54356158437356,-3.70372906392697));
#4944=CARTESIAN_POINT('Ctrl Pts',(3.81342725369011,-2.65620468295633,-3.66594310691183));
#4945=CARTESIAN_POINT('Ctrl Pts',(3.61393376345345,-2.7692906630002,-3.63348439979832));
#4946=CARTESIAN_POINT('Ctrl Pts',(3.42914532611981,-2.87404085565993,-3.60341828707324));
#4947=CARTESIAN_POINT('Ctrl Pts',(3.24403860215133,-2.97917130976551,-3.577923704644));
#4948=CARTESIAN_POINT('Ctrl Pts',(3.05874390643497,-3.08472586676541,-3.55771928043663));
#4949=CARTESIAN_POINT('Ctrl Pts',(2.88773569998093,-3.18214201462554,-3.53907264658248));
#4950=CARTESIAN_POINT('Ctrl Pts',(2.71656732320876,-3.27991952009122,-3.52493209277403));
#4951=CARTESIAN_POINT('Ctrl Pts',(2.54534428121679,-3.37808801310675,-3.51581971997351));
#4952=CARTESIAN_POINT('Ctrl Pts',(2.39699951098393,-3.46313954805832,-3.5079249130968));
#4953=CARTESIAN_POINT('Ctrl Pts',(2.24861371330972,-3.54848456051724,-3.50380398528744));
#4954=CARTESIAN_POINT('Ctrl Pts',(2.10025818716125,-3.63413792844054,-3.50376507030381));
#4955=CARTESIAN_POINT('Ctrl Pts',(2.0947836520027,-3.63729866256564,-3.50376363428419));
#4956=CARTESIAN_POINT('Ctrl Pts',(2.08930702825758,-3.64046099613376,-3.50376773690171));
#4957=CARTESIAN_POINT('Ctrl Pts',(2.08382833422878,-3.64362492389969,-3.50377740609618));
#4958=CARTESIAN_POINT('Ctrl Pts',(1.96293505333574,-3.71344039563817,-3.5039907672798));
#4959=CARTESIAN_POINT('Ctrl Pts',(1.84199090601466,-3.78347495065613,-3.5068800488842));
#4960=CARTESIAN_POINT('Ctrl Pts',(1.72115880571068,-3.85362529081441,-3.51232413713592));
#4961=CARTESIAN_POINT('Ctrl Pts',(1.59475077179073,-3.92701279757723,-3.51801944898314));
#4962=CARTESIAN_POINT('Ctrl Pts',(1.46846525155069,-4.00052698685701,-3.52651072880892));
#4963=CARTESIAN_POINT('Ctrl Pts',(1.34247226888016,-4.07405414400108,-3.53760308570294));
#4964=CARTESIAN_POINT('Ctrl Pts',(1.24270876420383,-4.13227426650394,-3.5463862129487));
#4965=CARTESIAN_POINT('Ctrl Pts',(1.14312828434623,-4.19050262268746,-3.55679891920022));
#4966=CARTESIAN_POINT('Ctrl Pts',(1.04380946022049,-4.24868470200342,-3.5687222525591));
#4967=CARTESIAN_POINT('Ctrl Pts',(0.864208532035138,-4.35389693685298,-3.59028354023209));
#4968=CARTESIAN_POINT('Ctrl Pts',(0.685256950144924,-4.45903161754731,-3.61679277506933));
#4969=CARTESIAN_POINT('Ctrl Pts',(0.506826534709686,-4.56402874599945,-3.64753780817784));
#4970=CARTESIAN_POINT('Ctrl Pts',(0.337456180068921,-4.66369449434636,-3.67672171804169));
#4971=CARTESIAN_POINT('Ctrl Pts',(0.168554912827431,-4.76323644283656,-3.7097209642112));
#4972=CARTESIAN_POINT('Ctrl Pts',(5.49614199430651E-12,-4.86260619450716,
-3.7458852558793));
#4973=CARTESIAN_POINT('',(-4.21114045006265,-2.43130307244757,-3.74588539224308));
#4974=CARTESIAN_POINT('Ctrl Pts',(1.79620807498344E-11,-4.86260604116954,
-3.74588567721565));
#4975=CARTESIAN_POINT('Ctrl Pts',(-0.196513977808605,-4.74675097482129,
-3.7037290639203));
#4976=CARTESIAN_POINT('Ctrl Pts',(-0.393627106302676,-4.63062721862453,
-3.66594310690113));
#4977=CARTESIAN_POINT('Ctrl Pts',(-0.591309182975744,-4.51440377819733,
-3.63348439978504));
#4978=CARTESIAN_POINT('Ctrl Pts',(-0.774419729558393,-4.40674739345823,
-3.60341828705788));
#4979=CARTESIAN_POINT('Ctrl Pts',(-0.958018735530767,-4.2990054951306,-3.57792370462771));
#4980=CARTESIAN_POINT('Ctrl Pts',(-1.14207901125747,-4.19131285994132,-3.55771928042079));
#4981=CARTESIAN_POINT('Ctrl Pts',(-1.31194797329025,-4.09192348281499,-3.53907264656702));
#4982=CARTESIAN_POINT('Ctrl Pts',(-1.48220996534842,-3.99257607292704,-3.52493209276015));
#4983=CARTESIAN_POINT('Ctrl Pts',(-1.65283789516731,-3.89337681534504,-3.51581971996257));
#4984=CARTESIAN_POINT('Ctrl Pts',(-1.80066707011438,-3.80743224332055,-3.507924913093));
#4985=CARTESIAN_POINT('Ctrl Pts',(-1.94877091775868,-3.72159887924319,-3.50380398528742));
#4986=CARTESIAN_POINT('Ctrl Pts',(-2.09712667330543,-3.63594590880816,-3.5037650703038));
#4987=CARTESIAN_POINT('Ctrl Pts',(-2.10260121693164,-3.6327851893495,-3.50376363428419));
#4988=CARTESIAN_POINT('Ctrl Pts',(-2.10807819000943,-3.62962346084331,-3.5037677369017));
#4989=CARTESIAN_POINT('Ctrl Pts',(-2.11355757884486,-3.62646073651777,-3.50377740609617));
#4990=CARTESIAN_POINT('Ctrl Pts',(-2.23446619139723,-3.55667181998499,-3.5039907672798));
#4991=CARTESIAN_POINT('Ctrl Pts',(-2.35558996884922,-3.48694839347305,-3.50688004888436));
#4992=CARTESIAN_POINT('Ctrl Pts',(-2.47675799566555,-3.41737989509451,-3.51232413713636));
#4993=CARTESIAN_POINT('Ctrl Pts',(-2.60351745780718,-3.34460107985613,-3.51801944898395));
#4994=CARTESIAN_POINT('Ctrl Pts',(-2.73032537338674,-3.27199170583537,-3.52651072881029));
#4995=CARTESIAN_POINT('Ctrl Pts',(-2.85699825068146,-3.19964216071353,-3.53760308570505));
#4996=CARTESIAN_POINT('Ctrl Pts',(-2.95730010811074,-3.14235449254917,-3.54638621295039));
#4997=CARTESIAN_POINT('Ctrl Pts',(-3.05751758370728,-3.08522944536764,-3.55679891920123));
#4998=CARTESIAN_POINT('Ctrl Pts',(-3.157564154495,-3.02830786026315,-3.56872225255918));
#4999=CARTESIAN_POINT('Ctrl Pts',(-3.33848108677305,-2.92537501132664,-3.59028354023417));
#5000=CARTESIAN_POINT('Ctrl Pts',(-3.51900618203487,-2.82296573570007,-3.6167927750743));
#5001=CARTESIAN_POINT('Ctrl Pts',(-3.69915157033305,-2.72093902734208,-3.64753780818642));
#5002=CARTESIAN_POINT('Ctrl Pts',(-3.87014981759516,-2.62409287175656,-3.67672171804863));
#5003=CARTESIAN_POINT('Ctrl Pts',(-4.04080630733679,-2.52759105784699,-3.70972096421582));
#5004=CARTESIAN_POINT('Ctrl Pts',(-4.21114049304847,-2.43130309725362,-3.7458852558811));
#5005=CARTESIAN_POINT('',(-4.19739387007612,1.49812671196668E-11,-3.50376779957655));
#5006=CARTESIAN_POINT('Ctrl Pts',(-4.21114036409982,-2.43130302282868,-3.7458856649686));
#5007=CARTESIAN_POINT('Ctrl Pts',(-4.20908206342616,-2.20517585842347,-3.70409596729133));
#5008=CARTESIAN_POINT('Ctrl Pts',(-4.20708960517473,-1.97840718425451,-3.66659889897082));
#5009=CARTESIAN_POINT('Ctrl Pts',(-4.20529095013208,-1.75110446615803,-3.63432933778681));
#5010=CARTESIAN_POINT('Ctrl Pts',(-4.2036243969318,-1.54049594852025,-3.6044298077561));
#5011=CARTESIAN_POINT('Ctrl Pts',(-4.20212438692378,-1.32942868276544,-3.57901881382086));
#5012=CARTESIAN_POINT('Ctrl Pts',(-4.20089156122566,-1.11799092190762,-3.55879847693247));
#5013=CARTESIAN_POINT('Ctrl Pts',(-4.19975422779664,-0.922930716764744,
-3.54014436782016));
#5014=CARTESIAN_POINT('Ctrl Pts',(-4.19884437084874,-0.727555053652698,
-3.52590816900496));
#5015=CARTESIAN_POINT('Ctrl Pts',(-4.1982384076207,-0.531938318567338,-3.51659854639054));
#5016=CARTESIAN_POINT('Ctrl Pts',(-4.1976896945174,-0.354803039069626,-3.50816847723974));
#5017=CARTESIAN_POINT('Ctrl Pts',(-4.19739018650638,-0.177470047501419,
-3.50377792009247));
#5018=CARTESIAN_POINT('Ctrl Pts',(-4.19739378314994,3.00402705630902E-11,
-3.50376803840416));
#5019=CARTESIAN_POINT('',(-4.21114047113314,2.43130308459242,-3.74588532543767));
#5020=CARTESIAN_POINT('Ctrl Pts',(-4.1973939570023,-7.77393595236366E-14,
-3.50376756074893));
#5021=CARTESIAN_POINT('Ctrl Pts',(-4.1973939570023,0.406987107455743,-3.50376756074893));
#5022=CARTESIAN_POINT('Ctrl Pts',(-4.19892854886077,0.815883880986007,-3.52647143761692));
#5023=CARTESIAN_POINT('Ctrl Pts',(-4.20401592436619,1.62672484819092,-3.61062719041339));
#5024=CARTESIAN_POINT('Ctrl Pts',(-4.20749145004057,2.02981982514647,-3.67167082875957));
#5025=CARTESIAN_POINT('Ctrl Pts',(-4.2111405601822,2.43130313601654,-3.74588504288743));
#5026=CARTESIAN_POINT('',(-9.51175986589573E-12,4.86260614339766,-3.74588539632585));
#5027=CARTESIAN_POINT('Ctrl Pts',(-4.21114036026505,2.43130302056491,-3.74588567721725));
#5028=CARTESIAN_POINT('Ctrl Pts',(-4.01254994075699,2.54356158437606,-3.70372906392602));
#5029=CARTESIAN_POINT('Ctrl Pts',(-3.81342725368073,2.65620468296162,-3.66594310691005));
#5030=CARTESIAN_POINT('Ctrl Pts',(-3.61393376343911,2.76929066300832,-3.633484399796));
#5031=CARTESIAN_POINT('Ctrl Pts',(-3.42914532610122,2.87404085567046,-3.60341828707046));
#5032=CARTESIAN_POINT('Ctrl Pts',(-3.24403860212847,2.97917130977849,-3.57792370464101));
#5033=CARTESIAN_POINT('Ctrl Pts',(-3.05874390640785,3.08472586678085,-3.55771928043369));
#5034=CARTESIAN_POINT('Ctrl Pts',(-2.88773569994925,3.18214201464361,-3.53907264657952));
#5035=CARTESIAN_POINT('Ctrl Pts',(-2.71656732317253,3.27991952011193,-3.52493209277131));
#5036=CARTESIAN_POINT('Ctrl Pts',(-2.54534428117601,3.37808801313014,-3.51581971997135));
#5037=CARTESIAN_POINT('Ctrl Pts',(-2.39699951095675,3.46313954807398,-3.50792491309605));
#5038=CARTESIAN_POINT('Ctrl Pts',(-2.24861371329614,3.5484845605251,-3.50380398528744));
#5039=CARTESIAN_POINT('Ctrl Pts',(-2.10025818716127,3.63413792844057,-3.50376507030382));
#5040=CARTESIAN_POINT('Ctrl Pts',(-2.09478365200272,3.63729866256567,-3.5037636342842));
#5041=CARTESIAN_POINT('Ctrl Pts',(-2.0893070282576,3.64046099613379,-3.50376773690172));
#5042=CARTESIAN_POINT('Ctrl Pts',(-2.0838283342288,3.64362492389971,-3.50377740609619));
#5043=CARTESIAN_POINT('Ctrl Pts',(-1.96293505333605,3.71344039563804,-3.50399076727982));
#5044=CARTESIAN_POINT('Ctrl Pts',(-1.84199090601524,3.78347495065584,-3.5068800488842));
#5045=CARTESIAN_POINT('Ctrl Pts',(-1.72115880571154,3.85362529081395,-3.51232413713589));
#5046=CARTESIAN_POINT('Ctrl Pts',(-1.59475077179095,3.92701279757712,-3.51801944898313));
#5047=CARTESIAN_POINT('Ctrl Pts',(-1.46846525155029,4.00052698685725,-3.52651072880895));
#5048=CARTESIAN_POINT('Ctrl Pts',(-1.34247226887913,4.07405414400167,-3.53760308570303));
#5049=CARTESIAN_POINT('Ctrl Pts',(-1.24270876420315,4.13227426650433,-3.54638621294877));
#5050=CARTESIAN_POINT('Ctrl Pts',(-1.14312828434588,4.19050262268764,-3.55679891920027));
#5051=CARTESIAN_POINT('Ctrl Pts',(-1.04380946022048,4.2486847020034,-3.56872225255911));
#5052=CARTESIAN_POINT('Ctrl Pts',(-0.864208532033562,4.35389693685388,-3.59028354023228));
#5053=CARTESIAN_POINT('Ctrl Pts',(-0.685256950141792,4.45903161754913,-3.61679277506979));
#5054=CARTESIAN_POINT('Ctrl Pts',(-0.506826534705005,4.56402874600219,-3.64753780817865));
#5055=CARTESIAN_POINT('Ctrl Pts',(-0.337456180063016,4.66369449434982,-3.67672171804278));
#5056=CARTESIAN_POINT('Ctrl Pts',(-0.1685549128203,4.76323644284074,-3.70972096421261));
#5057=CARTESIAN_POINT('Ctrl Pts',(2.85244410943447E-12,4.86260619451207,
-3.74588525588108));
#5058=CARTESIAN_POINT('',(4.21114044751304,2.43130307097638,-3.74588540033132));
#5059=CARTESIAN_POINT('Ctrl Pts',(-2.02518052867876E-11,4.86260604117087,
-3.74588567721613));
#5060=CARTESIAN_POINT('Ctrl Pts',(0.19651397780476,4.74675097482353,-3.70372906392109));
#5061=CARTESIAN_POINT('Ctrl Pts',(0.393627106297267,4.63062721862769,-3.66594310690214));
#5062=CARTESIAN_POINT('Ctrl Pts',(0.591309182968762,4.51440377820141,-3.63348439978618));
#5063=CARTESIAN_POINT('Ctrl Pts',(0.774419729549811,4.40674739346324,-3.60341828705915));
#5064=CARTESIAN_POINT('Ctrl Pts',(0.958018735520578,4.29900549513656,-3.57792370462905));
#5065=CARTESIAN_POINT('Ctrl Pts',(1.14207901124566,4.19131285994821,-3.55771928042208));
#5066=CARTESIAN_POINT('Ctrl Pts',(1.31194797327675,4.09192348282286,-3.53907264656829));
#5067=CARTESIAN_POINT('Ctrl Pts',(1.48220996533321,3.9925760729359,-3.52493209276128));
#5068=CARTESIAN_POINT('Ctrl Pts',(1.65283789515039,3.89337681535487,-3.51581971996347));
#5069=CARTESIAN_POINT('Ctrl Pts',(1.80066707010309,3.8074322433271,-3.50792491309331));
#5070=CARTESIAN_POINT('Ctrl Pts',(1.94877091775302,3.72159887924647,-3.50380398528742));
#5071=CARTESIAN_POINT('Ctrl Pts',(2.09712667330543,3.63594590880817,-3.50376507030381));
#5072=CARTESIAN_POINT('Ctrl Pts',(2.10260121693165,3.63278518934951,-3.50376363428419));
#5073=CARTESIAN_POINT('Ctrl Pts',(2.10807819000944,3.62962346084332,-3.50376773690171));
#5074=CARTESIAN_POINT('Ctrl Pts',(2.11355757884487,3.62646073651778,-3.50377740609618));
#5075=CARTESIAN_POINT('Ctrl Pts',(2.23446619139685,3.55667181998522,-3.50399076727981));
#5076=CARTESIAN_POINT('Ctrl Pts',(2.35558996884845,3.48694839347351,-3.50688004888434));
#5077=CARTESIAN_POINT('Ctrl Pts',(2.47675799566439,3.41737989509519,-3.51232413713631));
#5078=CARTESIAN_POINT('Ctrl Pts',(2.60351745780486,3.34460107985747,-3.51801944898383));
#5079=CARTESIAN_POINT('Ctrl Pts',(2.73032537338327,3.27199170583736,-3.52651072881004));
#5080=CARTESIAN_POINT('Ctrl Pts',(2.85699825067684,3.19964216071616,-3.53760308570463));
#5081=CARTESIAN_POINT('Ctrl Pts',(2.95730010810766,3.14235449255091,-3.54638621295005));
#5082=CARTESIAN_POINT('Ctrl Pts',(3.05751758370574,3.0852294453685,-3.55679891920103));
#5083=CARTESIAN_POINT('Ctrl Pts',(3.157564154495,3.02830786026314,-3.56872225255917));
#5084=CARTESIAN_POINT('Ctrl Pts',(3.33848108677087,2.92537501132787,-3.59028354023389));
#5085=CARTESIAN_POINT('Ctrl Pts',(3.51900618203053,2.82296573570252,-3.61679277507365));
#5086=CARTESIAN_POINT('Ctrl Pts',(3.69915157032656,2.72093902734574,-3.6475378081853));
#5087=CARTESIAN_POINT('Ctrl Pts',(3.87014981758778,2.62409287176072,-3.67672171804727));
#5088=CARTESIAN_POINT('Ctrl Pts',(4.04080630732854,2.52759105785164,-3.70972096421418));
#5089=CARTESIAN_POINT('Ctrl Pts',(4.21114049303935,2.43130309725876,-3.74588525587916));
#5090=CARTESIAN_POINT('Ctrl Pts',(4.21114035645151,2.43130301841489,-3.74588568923342));
#5091=CARTESIAN_POINT('Ctrl Pts',(4.20904504440769,2.20112279744945,-3.70334735266769));
#5092=CARTESIAN_POINT('Ctrl Pts',(4.20701816094358,1.97027747715211,-3.66526171181474));
#5093=CARTESIAN_POINT('Ctrl Pts',(4.20519448587801,1.73888075176048,-3.63260836994925));
#5094=CARTESIAN_POINT('Ctrl Pts',(4.2035056635924,1.52459480025731,-3.60236959963146));
#5095=CARTESIAN_POINT('Ctrl Pts',(4.20199126981785,1.30983574967937,-3.57679014301546));
#5096=CARTESIAN_POINT('Ctrl Pts',(4.20075710188212,1.09469708220331,-3.55660623332013));
#5097=CARTESIAN_POINT('Ctrl Pts',(4.19961779997554,0.896095346621634,-3.53797378782187));
#5098=CARTESIAN_POINT('Ctrl Pts',(4.19871737958875,0.697169997202399,-3.52393953141141));
#5099=CARTESIAN_POINT('Ctrl Pts',(4.1981363871834,0.497999620803157,-3.51503969854886));
#5100=CARTESIAN_POINT('Ctrl Pts',(4.19765260282079,0.332153195431398,-3.50762893047509));
#5101=CARTESIAN_POINT('Ctrl Pts',(4.19739028041404,0.166136914123517,-3.50377766208245));
#5102=CARTESIAN_POINT('Ctrl Pts',(4.19739377366243,-3.28756114544519E-11,
-3.50376806447087));
#5103=CARTESIAN_POINT('Origin',(0.,0.,-4.));
#5104=CARTESIAN_POINT('Origin',(0.,0.,-4.48445439793712));
#5105=CARTESIAN_POINT('',(-5.38445439793712,-6.59405484358858E-16,-5.));
#5106=CARTESIAN_POINT('Origin',(-5.38445439793712,-6.59405484358858E-16,
-4.48445439793712));
#5107=CARTESIAN_POINT('Origin',(0.,0.,-5.));
#5108=CARTESIAN_POINT('Origin',(0.,0.,-5.));
#5109=CARTESIAN_POINT('',(-2.1,-2.57175827820944E-16,-5.));
#5110=CARTESIAN_POINT('Origin',(1.56747850547613E-15,4.61880215351701,-5.));
#5111=CARTESIAN_POINT('',(1.09700060671018E-7,4.61880068173267,-3.43332218935783));
#5112=CARTESIAN_POINT('',(1.73472347597681E-15,4.61880215351701,-0.5));
#5113=CARTESIAN_POINT('',(1.56747850547613E-15,4.61880215351701,-5.));
#5114=CARTESIAN_POINT('',(-4.00000000017049,2.30939825730392,-3.43332219680665));
#5115=CARTESIAN_POINT('Ctrl Pts',(-2.43977409528084E-6,4.61880074491278,
-3.4333119175934));
#5116=CARTESIAN_POINT('Ctrl Pts',(-0.16663428147485,4.52259580625129,-3.40020822163793));
#5117=CARTESIAN_POINT('Ctrl Pts',(-0.333219628702097,4.42641771117134,-3.37037814524522));
#5118=CARTESIAN_POINT('Ctrl Pts',(-0.499799729884962,4.33024264503938,-3.34429832550047));
#5119=CARTESIAN_POINT('Ctrl Pts',(-0.664211398942607,4.23531952377698,-3.31855799599827));
#5120=CARTESIAN_POINT('Ctrl Pts',(-0.82861798209483,4.14039933903518,-3.29647105632394));
#5121=CARTESIAN_POINT('Ctrl Pts',(-0.993047089653662,4.0454661498736,-3.27844793346592));
#5122=CARTESIAN_POINT('Ctrl Pts',(-1.15827103668867,3.95007405992818,-3.26033768801905));
#5123=CARTESIAN_POINT('Ctrl Pts',(-1.32351778079621,3.8546688081062,-3.24633089903767));
#5124=CARTESIAN_POINT('Ctrl Pts',(-1.48880246969282,3.75924164848933,-3.23679221713863));
#5125=CARTESIAN_POINT('Ctrl Pts',(-1.65408715858944,3.66381448887247,-3.22725353523959));
#5126=CARTESIAN_POINT('Ctrl Pts',(-1.81940985241266,3.56836538664265,-3.22218315324263));
#5127=CARTESIAN_POINT('Ctrl Pts',(-1.98477204010767,3.47289348249879,-3.22189077969918));
#5128=CARTESIAN_POINT('Ctrl Pts',(-1.98984970207412,3.46996189297828,-3.22188180198764));
#5129=CARTESIAN_POINT('Ctrl Pts',(-1.99492568895773,3.46703127056732,-3.22187739028159));
#5130=CARTESIAN_POINT('Ctrl Pts',(-2.00000000019057,3.46410161559385,-3.22187752539236));
#5131=CARTESIAN_POINT('Ctrl Pts',(-2.20332030962145,3.34671457952159,-3.22188293908513));
#5132=CARTESIAN_POINT('Ctrl Pts',(-2.40664181574471,3.22932685336206,-3.22920718089928));
#5133=CARTESIAN_POINT('Ctrl Pts',(-2.60996148300162,3.11194018873347,-3.24317060794845));
#5134=CARTESIAN_POINT('Ctrl Pts',(-2.73997359254122,3.03687766228887,-3.25209947661895));
#5135=CARTESIAN_POINT('Ctrl Pts',(-2.86998504929241,2.96181551273783,-3.26374198223858));
#5136=CARTESIAN_POINT('Ctrl Pts',(-2.99999613197012,2.88675357915622,-3.27790934942572));
#5137=CARTESIAN_POINT('Ctrl Pts',(-3.20876161260061,2.7662227727167,-3.30065861940469));
#5138=CARTESIAN_POINT('Ctrl Pts',(-3.41752306189258,2.64569429377157,-3.32992036801802));
#5139=CARTESIAN_POINT('Ctrl Pts',(-3.62629054976681,2.52516232844934,-3.36487326410363));
#5140=CARTESIAN_POINT('Ctrl Pts',(-3.75085541086908,2.45324477236037,-3.38572853563255));
#5141=CARTESIAN_POINT('Ctrl Pts',(-3.87542250422839,2.38132592747721,-3.40860890830996));
#5142=CARTESIAN_POINT('Ctrl Pts',(-3.99999468199604,2.30940414710952,-3.43333114741226));
#5143=CARTESIAN_POINT('',(-4.,2.3094010767585,-0.499999999999993));
#5144=CARTESIAN_POINT('',(-4.,2.3094010767585,-5.));
#5145=CARTESIAN_POINT('',(-2.00000000000001,3.46410161513775,0.));
#5146=CARTESIAN_POINT('Ctrl Pts',(-4.,2.3094010767585,-0.499999999999992));
#5147=CARTESIAN_POINT('Ctrl Pts',(-2.92820323027552,2.9282032302755,-1.16573417585641E-15));
#5148=CARTESIAN_POINT('Ctrl Pts',(-2.00000000000001,3.46410161513775,5.26836153967997E-16));
#5149=CARTESIAN_POINT('Ctrl Pts',(-2.00000000000001,3.46410161513775,5.26836153967997E-16));
#5150=CARTESIAN_POINT('Ctrl Pts',(-1.0717967697245,4.,2.26437397702801E-15));
#5151=CARTESIAN_POINT('Ctrl Pts',(1.41896768074064E-16,4.61880215351701,
-0.499999999999997));
#5152=CARTESIAN_POINT('Origin',(4.,2.3094010767585,-5.));
#5153=CARTESIAN_POINT('',(3.99999878025273,2.3094002216274,-3.43332248801257));
#5154=CARTESIAN_POINT('',(4.,2.30940107675852,-0.5));
#5155=CARTESIAN_POINT('',(4.,2.3094010767585,-5.));
#5156=CARTESIAN_POINT('Ctrl Pts',(3.9999975602259,2.30940248536273,-3.43331191759338));
#5157=CARTESIAN_POINT('Ctrl Pts',(3.83336571851849,2.40560742402807,-3.40020822163658));
#5158=CARTESIAN_POINT('Ctrl Pts',(3.66678037127137,2.50178551908899,-3.37037814524283));
#5159=CARTESIAN_POINT('Ctrl Pts',(3.50020027019235,2.5979605854162,-3.34429832549734));
#5160=CARTESIAN_POINT('Ctrl Pts',(3.33578860123532,2.6928837068724,-3.31855799599412));
#5161=CARTESIAN_POINT('Ctrl Pts',(3.17138201833244,2.78780389206561,-3.29647105631917));
#5162=CARTESIAN_POINT('Ctrl Pts',(3.00695291106838,2.88273708175725,-3.27844793346097));
#5163=CARTESIAN_POINT('Ctrl Pts',(2.84172896434559,2.97812917222605,-3.26033768801568));
#5164=CARTESIAN_POINT('Ctrl Pts',(2.67648222056708,3.07353442460049,-3.24633089903554));
#5165=CARTESIAN_POINT('Ctrl Pts',(2.51119753168713,3.16896158422877,-3.23679221713734));
#5166=CARTESIAN_POINT('Ctrl Pts',(2.34591284280719,3.26438874385705,-3.22725353523913));
#5167=CARTESIAN_POINT('Ctrl Pts',(2.18059014860371,3.35983784541075,-3.22218315324262));
#5168=CARTESIAN_POINT('Ctrl Pts',(2.01522796042752,3.45530974870371,-3.22189077969918));
#5169=CARTESIAN_POINT('Ctrl Pts',(2.01015029844606,3.45824133819823,-3.22188180198763));
#5170=CARTESIAN_POINT('Ctrl Pts',(2.00507431154748,3.46117196058322,-3.22187739028159));
#5171=CARTESIAN_POINT('Ctrl Pts',(2.00000000029971,3.46410161553084,-3.22187752539235));
#5172=CARTESIAN_POINT('Ctrl Pts',(1.79667969023904,3.58148865058546,-3.22188293908513));
#5173=CARTESIAN_POINT('Ctrl Pts',(1.59335818419909,3.69887637696245,-3.22920718090153));
#5174=CARTESIAN_POINT('Ctrl Pts',(1.39003851690507,3.81626304159993,-3.2431706079549));
#5175=CARTESIAN_POINT('Ctrl Pts',(1.26002640739368,3.89132556802023,-3.25209947662451));
#5176=CARTESIAN_POINT('Ctrl Pts',(1.1300149506759,3.96638771755598,-3.26374198224188));
#5177=CARTESIAN_POINT('Ctrl Pts',(1.00000386802987,4.0414496511193,-3.27790934942554));
#5178=CARTESIAN_POINT('Ctrl Pts',(0.791238387378459,4.16198045757089,-3.30065861940672));
#5179=CARTESIAN_POINT('Ctrl Pts',(0.582476938065581,4.2825089365281,-3.32992036802359));
#5180=CARTESIAN_POINT('Ctrl Pts',(0.373709450170437,4.4030409018624,-3.36487326411387));
#5181=CARTESIAN_POINT('Ctrl Pts',(0.249144589089073,4.4749584579393,-3.38572853563997));
#5182=CARTESIAN_POINT('Ctrl Pts',(0.124577495750671,4.54687730281039,-3.40860890831389));
#5183=CARTESIAN_POINT('Ctrl Pts',(5.31800394343307E-6,4.618799083166,-3.43333114741212));
#5184=CARTESIAN_POINT('',(2.00000000000001,3.46410161513775,0.));
#5185=CARTESIAN_POINT('Ctrl Pts',(4.82449011451827E-15,4.61880215351701,
-0.499999999999999));
#5186=CARTESIAN_POINT('Ctrl Pts',(1.0717967697245,4.,-1.11022302462516E-15));
#5187=CARTESIAN_POINT('Ctrl Pts',(2.00000000000001,3.46410161513775,-1.44879942341204E-15));
#5188=CARTESIAN_POINT('Ctrl Pts',(2.00000000000001,3.46410161513775,-1.44879942341204E-15));
#5189=CARTESIAN_POINT('Ctrl Pts',(2.92820323027551,2.92820323027551,-1.86623997575081E-15));
#5190=CARTESIAN_POINT('Ctrl Pts',(3.99999999999999,2.3094010767585,-0.499999999999988));
#5191=CARTESIAN_POINT('Origin',(4.,2.3094010767585,-5.));
#5192=CARTESIAN_POINT('',(3.99999867054726,-2.30940043459921,-3.43332219625534));
#5193=CARTESIAN_POINT('',(4.,-2.30940107675852,-0.5));
#5194=CARTESIAN_POINT('',(4.,-2.30940107675851,-5.));
#5195=CARTESIAN_POINT('Ctrl Pts',(4.,-2.30939825700977,-3.43331193230041));
#5196=CARTESIAN_POINT('Ctrl Pts',(4.,-2.11694957105523,-3.40020158541481));
#5197=CARTESIAN_POINT('Ctrl Pts',(3.99999999998634,-1.92455454067137,-3.37036624965622));
#5198=CARTESIAN_POINT('Ctrl Pts',(4.00000000010068,-1.73216556308653,-3.34428277264658));
#5199=CARTESIAN_POINT('Ctrl Pts',(4.00000000021354,-1.54228190072953,-3.31853895819436));
#5200=CARTESIAN_POINT('Ctrl Pts',(4.00000000048029,-1.35240410653802,-3.29645005892505));
#5201=CARTESIAN_POINT('Ctrl Pts',(4.00000000079391,-1.16250031290758,-3.27842669391039));
#5202=CARTESIAN_POINT('Ctrl Pts',(4.00000000110889,-0.971775122729002,-3.26032537189695));
#5203=CARTESIAN_POINT('Ctrl Pts',(4.00000000144109,-0.781023646483771,-3.2463250813576));
#5204=CARTESIAN_POINT('Ctrl Pts',(4.00000000145045,-0.590228413801205,-3.236790121837));
#5205=CARTESIAN_POINT('Ctrl Pts',(4.00000000145981,-0.399433181118639,-3.2272551623164));
#5206=CARTESIAN_POINT('Ctrl Pts',(4.00000000105901,-0.208594122424576,-3.22218572635334));
#5207=CARTESIAN_POINT('Ctrl Pts',(4.00000000055376,-0.0177094910373128,
-3.22189127571074));
#5208=CARTESIAN_POINT('Ctrl Pts',(4.00000000053813,-0.0118043805065834,
-3.2218821667344));
#5209=CARTESIAN_POINT('Ctrl Pts',(4.00000000052252,-0.0059012165529552,
-3.22187769126366));
#5210=CARTESIAN_POINT('Ctrl Pts',(4.00000000050698,-6.5066340334549E-11,
-3.2218778296733));
#5211=CARTESIAN_POINT('Ctrl Pts',(3.99999999987799,0.238764894989697,-3.22188342976665));
#5212=CARTESIAN_POINT('Ctrl Pts',(4.00000000000652,0.477530878358765,-3.22946180827315));
#5213=CARTESIAN_POINT('Ctrl Pts',(4.00000000000153,0.716294821461492,-3.24389360090326));
#5214=CARTESIAN_POINT('Ctrl Pts',(3.99999999999847,0.862428932159365,-3.25272649733801));
#5215=CARTESIAN_POINT('Ctrl Pts',(4.,1.00856237380136,-3.26412563955697));
#5216=CARTESIAN_POINT('Ctrl Pts',(4.,1.1546953597049,-3.27791652926043));
#5217=CARTESIAN_POINT('Ctrl Pts',(4.,1.3986057399827,-3.30093488566466));
#5218=CARTESIAN_POINT('Ctrl Pts',(4.,1.64251152018096,-3.33061880975289));
#5219=CARTESIAN_POINT('Ctrl Pts',(4.,1.88642485026101,-3.36611862393459));
#5220=CARTESIAN_POINT('Ctrl Pts',(4.,2.02741126626355,-3.38663817310639));
#5221=CARTESIAN_POINT('Ctrl Pts',(4.,2.16840027918935,-3.4090998642691));
#5222=CARTESIAN_POINT('Ctrl Pts',(4.,2.30939483911209,-3.43333170804235));
#5223=CARTESIAN_POINT('',(4.,0.,0.));
#5224=CARTESIAN_POINT('Ctrl Pts',(4.,-2.10734454975715E-15,2.63418068719643E-16));
#5225=CARTESIAN_POINT('Ctrl Pts',(4.,1.07179676972449,7.12431934417829E-16));
#5226=CARTESIAN_POINT('Ctrl Pts',(4.,2.3094010767585,-0.499999999999993));
#5227=CARTESIAN_POINT('Ctrl Pts',(4.,-2.30940107675851,-0.499999999999998));
#5228=CARTESIAN_POINT('Ctrl Pts',(4.,-1.0717967697245,-3.33066907387547E-16));
#5229=CARTESIAN_POINT('Ctrl Pts',(4.,-2.10734454975715E-15,2.63418068719643E-16));
#5230=CARTESIAN_POINT('Origin',(-6.25964416140486E-16,-4.61880215351703,
-5.));
#5231=CARTESIAN_POINT('',(-1.09700057365134E-7,-4.61880068173268,-3.43332218935784));
#5232=CARTESIAN_POINT('',(-2.68882138776405E-14,-4.61880215351701,-0.5));
#5233=CARTESIAN_POINT('',(-6.25964416140486E-16,-4.61880215351703,-5.));
#5234=CARTESIAN_POINT('Ctrl Pts',(2.43977409417062E-6,-4.6188007449128,
-3.43331191759339));
#5235=CARTESIAN_POINT('Ctrl Pts',(0.166634281473495,-4.52259580625208,-3.40020822163818));
#5236=CARTESIAN_POINT('Ctrl Pts',(0.333219628699384,-4.42641771117292,-3.37037814524569));
#5237=CARTESIAN_POINT('Ctrl Pts',(0.499799729880895,-4.33024264504174,-3.34429832550108));
#5238=CARTESIAN_POINT('Ctrl Pts',(0.664211398937362,-4.23531952378002,-3.318557995999));
#5239=CARTESIAN_POINT('Ctrl Pts',(0.828617982088412,-4.1403993390389,-3.29647105632474));
#5240=CARTESIAN_POINT('Ctrl Pts',(0.993047089646068,-4.045466149878,-3.27844793346673));
#5241=CARTESIAN_POINT('Ctrl Pts',(1.15827103668234,-3.95007405993185,-3.2603376880196));
#5242=CARTESIAN_POINT('Ctrl Pts',(1.32351778079115,-3.85466880810913,-3.24633089903802));
#5243=CARTESIAN_POINT('Ctrl Pts',(1.48880246968903,-3.75924164849154,-3.23679221713884));
#5244=CARTESIAN_POINT('Ctrl Pts',(1.65408715858691,-3.66381448887394,-3.22725353523966));
#5245=CARTESIAN_POINT('Ctrl Pts',(1.8194098524114,-3.56836538664339,-3.22218315324264));
#5246=CARTESIAN_POINT('Ctrl Pts',(1.98477204010769,-3.4728934824988,-3.22189077969918));
#5247=CARTESIAN_POINT('Ctrl Pts',(1.98984970207413,-3.46996189297829,-3.22188180198764));
#5248=CARTESIAN_POINT('Ctrl Pts',(1.99492568895772,-3.46703127056734,-3.2218773902816));
#5249=CARTESIAN_POINT('Ctrl Pts',(2.00000000019056,-3.46410161559387,-3.22187752539236));
#5250=CARTESIAN_POINT('Ctrl Pts',(2.203320309618,-3.3467145795236,-3.22188293908513));
#5251=CARTESIAN_POINT('Ctrl Pts',(2.40664181573781,-3.22932685336607,-3.22920718089901));
#5252=CARTESIAN_POINT('Ctrl Pts',(2.60996148299126,-3.11194018873947,-3.2431706079477));
#5253=CARTESIAN_POINT('Ctrl Pts',(2.73997359253431,-3.03687766229287,-3.25209947661828));
#5254=CARTESIAN_POINT('Ctrl Pts',(2.86998504928896,-2.96181551273984,-3.26374198223814));
#5255=CARTESIAN_POINT('Ctrl Pts',(2.99999613197013,-2.88675357915623,-3.27790934942565));
#5256=CARTESIAN_POINT('Ctrl Pts',(3.20876161259695,-2.76622277271884,-3.30065861940419));
#5257=CARTESIAN_POINT('Ctrl Pts',(3.41752306188524,-2.64569429377582,-3.32992036801689));
#5258=CARTESIAN_POINT('Ctrl Pts',(3.62629054975579,-2.52516232845572,-3.3648732641017));
#5259=CARTESIAN_POINT('Ctrl Pts',(3.75085541086174,-2.45324477236463,-3.38572853563112));
#5260=CARTESIAN_POINT('Ctrl Pts',(3.87542250422473,-2.38132592747934,-3.40860890830916));
#5261=CARTESIAN_POINT('Ctrl Pts',(3.99999468199605,-2.30940414710953,-3.43333114741222));
#5262=CARTESIAN_POINT('',(2.00000000000001,-3.46410161513775,0.));
#5263=CARTESIAN_POINT('Ctrl Pts',(4.,-2.30940107675852,-0.499999999999999));
#5264=CARTESIAN_POINT('Ctrl Pts',(2.92820323027552,-2.92820323027552,-1.2267964422108E-14));
#5265=CARTESIAN_POINT('Ctrl Pts',(2.00000000000001,-3.46410161513777,-1.21172315412642E-14));
#5266=CARTESIAN_POINT('Ctrl Pts',(2.00000000000001,-3.46410161513777,-1.21172315412642E-14));
#5267=CARTESIAN_POINT('Ctrl Pts',(1.0717967697245,-4.00000000000002,-1.21572333146255E-14));
#5268=CARTESIAN_POINT('Ctrl Pts',(-7.09483840370325E-16,-4.61880215351703,
-0.500000000000012));
#5269=CARTESIAN_POINT('Origin',(-4.,-2.30940107675851,-5.));
#5270=CARTESIAN_POINT('',(-3.99999878024205,-2.30940027055269,-3.43332188511301));
#5271=CARTESIAN_POINT('',(-4.,-2.30940107675852,-0.5));
#5272=CARTESIAN_POINT('',(-4.,-2.30940107675851,-5.));
#5273=CARTESIAN_POINT('Ctrl Pts',(-3.99999756022589,-2.30940248536275,-3.43331191759346));
#5274=CARTESIAN_POINT('Ctrl Pts',(-3.83336571851771,-2.40560742402853,-3.40020822163657));
#5275=CARTESIAN_POINT('Ctrl Pts',(-3.66678037126983,-2.50178551908989,-3.37037814524273));
#5276=CARTESIAN_POINT('Ctrl Pts',(-3.50020027019005,-2.59796058541755,-3.34429832549716));
#5277=CARTESIAN_POINT('Ctrl Pts',(-3.33578860123178,-2.69288370687446,-3.31855799599379));
#5278=CARTESIAN_POINT('Ctrl Pts',(-3.17138201832767,-2.78780389206838,-3.29647105631872));
#5279=CARTESIAN_POINT('Ctrl Pts',(-3.00695291106237,-2.88273708176073,-3.27844793346046));
#5280=CARTESIAN_POINT('Ctrl Pts',(-2.84172896434058,-2.97812917222895,-3.26033768801535));
#5281=CARTESIAN_POINT('Ctrl Pts',(-2.67648222056308,-3.07353442460281,-3.24633089903534));
#5282=CARTESIAN_POINT('Ctrl Pts',(-2.51119753168413,-3.16896158423052,-3.23679221713722));
#5283=CARTESIAN_POINT('Ctrl Pts',(-2.34591284280519,-3.26438874385822,-3.2272535352391));
#5284=CARTESIAN_POINT('Ctrl Pts',(-2.1805901486027,-3.35983784541135,-3.22218315324262));
#5285=CARTESIAN_POINT('Ctrl Pts',(-2.01522796042751,-3.45530974870373,-3.22189077969918));
#5286=CARTESIAN_POINT('Ctrl Pts',(-2.01015029844606,-3.45824133819825,-3.22188180198764));
#5287=CARTESIAN_POINT('Ctrl Pts',(-2.00507431154748,-3.46117196058324,-3.2218773902816));
#5288=CARTESIAN_POINT('Ctrl Pts',(-2.00000000029972,-3.46410161553085,-3.22187752539236));
#5289=CARTESIAN_POINT('Ctrl Pts',(-1.79667969023426,-3.58148865058824,-3.22188293908513));
#5290=CARTESIAN_POINT('Ctrl Pts',(-1.59335818418951,-3.69887637696799,-3.22920718090189));
#5291=CARTESIAN_POINT('Ctrl Pts',(-1.39003851689071,-3.81626304160823,-3.24317060795591));
#5292=CARTESIAN_POINT('Ctrl Pts',(-1.2600264073841,-3.89132556802577,-3.25209947662539));
#5293=CARTESIAN_POINT('Ctrl Pts',(-1.13001495067111,-3.96638771755876,-3.26374198224244));
#5294=CARTESIAN_POINT('Ctrl Pts',(-1.00000386802987,-4.04144965111931,-3.27790934942557));
#5295=CARTESIAN_POINT('Ctrl Pts',(-0.79123838737471,-4.16198045757307,-3.30065861940717));
#5296=CARTESIAN_POINT('Ctrl Pts',(-0.582476938058081,-4.28250893653244,
-3.32992036802469));
#5297=CARTESIAN_POINT('Ctrl Pts',(-0.373709450159184,-4.40304090186891,
-3.36487326411579));
#5298=CARTESIAN_POINT('Ctrl Pts',(-0.24914458908157,-4.47495845794364,-3.38572853564138));
#5299=CARTESIAN_POINT('Ctrl Pts',(-0.124577495746921,-4.54687730281257,
-3.40860890831466));
#5300=CARTESIAN_POINT('Ctrl Pts',(-5.31800394298898E-6,-4.61879908316602,
-3.43333114741214));
#5301=CARTESIAN_POINT('',(-2.00000000000001,-3.46410161513775,0.));
#5302=CARTESIAN_POINT('Ctrl Pts',(-2.7811766542517E-14,-4.61880215351701,
-0.499999999999999));
#5303=CARTESIAN_POINT('Ctrl Pts',(-1.07179676972451,-4.00000000000001,-1.11022302462516E-14));
#5304=CARTESIAN_POINT('Ctrl Pts',(-2.00000000000001,-3.46410161513776,-1.08001411563443E-14));
#5305=CARTESIAN_POINT('Ctrl Pts',(-2.00000000000001,-3.46410161513776,-1.08001411563443E-14));
#5306=CARTESIAN_POINT('Ctrl Pts',(-2.92820323027552,-2.92820323027552,-1.05539304160516E-14));
#5307=CARTESIAN_POINT('Ctrl Pts',(-4.00000000000001,-2.30940107675851,-0.500000000000001));
#5308=CARTESIAN_POINT('Origin',(-4.,2.3094010767585,-5.));
#5309=CARTESIAN_POINT('Ctrl Pts',(-4.,2.30939825683146,-3.43331193331253));
#5310=CARTESIAN_POINT('Ctrl Pts',(-4.,2.11697930046273,-3.40020670375471));
#5311=CARTESIAN_POINT('Ctrl Pts',(-3.99999999998728,1.9246139805551,-3.37037536084733));
#5312=CARTESIAN_POINT('Ctrl Pts',(-4.0000000000937,1.73225470564797,-3.34429462341928));
#5313=CARTESIAN_POINT('Ctrl Pts',(-4.00000000019874,1.54240087817937,-3.31855358324167));
#5314=CARTESIAN_POINT('Ctrl Pts',(-4.000000000447,1.352552910853,-3.29646621734035));
#5315=CARTESIAN_POINT('Ctrl Pts',(-4.00000000073897,1.16267895982991,-3.27844302243925));
#5316=CARTESIAN_POINT('Ctrl Pts',(-4.00000000103237,0.971876565599027,-3.26033169795114));
#5317=CARTESIAN_POINT('Ctrl Pts',(-4.00000000134192,0.781047869753778,-3.24632464433699));
#5318=CARTESIAN_POINT('Ctrl Pts',(-4.00000000135058,0.590175421017146,-3.23678664305403));
#5319=CARTESIAN_POINT('Ctrl Pts',(-4.00000000135925,0.399302972280514,-3.22724864177108));
#5320=CARTESIAN_POINT('Ctrl Pts',(-4.00000000098556,0.208386701389507,-3.2221798857123));
#5321=CARTESIAN_POINT('Ctrl Pts',(-4.00000000051493,0.017424937160016,-3.22189020190631));
#5322=CARTESIAN_POINT('Ctrl Pts',(-4.00000000050061,0.0116147111477252,
-3.22188138795137));
#5323=CARTESIAN_POINT('Ctrl Pts',(-4.00000000048631,0.00580639863921593,
-3.2218770559679));
#5324=CARTESIAN_POINT('Ctrl Pts',(-4.00000000047207,6.06586074236706E-11,
-3.22187718730854));
#5325=CARTESIAN_POINT('Ctrl Pts',(-3.99999999990536,-0.231030142290403,
-3.22188241320624));
#5326=CARTESIAN_POINT('Ctrl Pts',(-4.00000000000776,-0.462061954876961,
-3.22897203276302));
#5327=CARTESIAN_POINT('Ctrl Pts',(-4.00000000000194,-0.693091561426993,
-3.24250253777789));
#5328=CARTESIAN_POINT('Ctrl Pts',(-3.99999999999807,-0.846960671690658,
-3.25151405279168));
#5329=CARTESIAN_POINT('Ctrl Pts',(-4.,-1.00082893608218,-3.26338147840436));
#5330=CARTESIAN_POINT('Ctrl Pts',(-4.,-1.1546967992463,-3.27790201754606));
#5331=CARTESIAN_POINT('Ctrl Pts',(-4.,-1.39301162222072,-3.30039183214339));
#5332=CARTESIAN_POINT('Ctrl Pts',(-4.,-1.63132173464497,-3.32924825001008));
#5333=CARTESIAN_POINT('Ctrl Pts',(-4.,-1.86963826834349,-3.3636766457411));
#5334=CARTESIAN_POINT('Ctrl Pts',(-4.,-2.01622009482115,-3.38485258788254));
#5335=CARTESIAN_POINT('Ctrl Pts',(-4.,-2.16280446588197,-3.40813542735712));
#5336=CARTESIAN_POINT('Ctrl Pts',(-4.,-2.30939503481467,-3.43333057628833));
#5337=CARTESIAN_POINT('',(-4.,0.,0.));
#5338=CARTESIAN_POINT('Ctrl Pts',(-4.,-2.30940107675851,-0.499999999999998));
#5339=CARTESIAN_POINT('Ctrl Pts',(-4.,-1.07179676972449,1.33226762955019E-15));
#5340=CARTESIAN_POINT('Ctrl Pts',(-4.,2.1073447210992E-15,7.90254270412198E-16));
#5341=CARTESIAN_POINT('Ctrl Pts',(-4.,2.1073447210992E-15,7.90254270412198E-16));
#5342=CARTESIAN_POINT('Ctrl Pts',(-4.,1.07179676972449,2.71717901185061E-16));
#5343=CARTESIAN_POINT('Ctrl Pts',(-4.,2.3094010767585,-0.499999999999992));
#5344=CARTESIAN_POINT('Origin',(8.67361737988404E-16,4.61880215351701,0.));
#5345=CARTESIAN_POINT('Origin',(0.,0.,0.));
#5346=CARTESIAN_POINT('Origin',(0.,0.,0.));
#5347=CARTESIAN_POINT('Origin',(0.,0.,0.));
#5348=CARTESIAN_POINT('Origin',(0.,0.,0.));
#5349=CARTESIAN_POINT('Origin',(0.,0.,0.));
#5350=CARTESIAN_POINT('Origin',(0.,0.,0.));
#5351=CARTESIAN_POINT('Origin',(8.67361737988404E-16,4.61880215351701,-5.));
#5352=CARTESIAN_POINT('Origin',(0.,0.,0.));
#5353=CARTESIAN_POINT('Origin',(0.,0.,0.));
#5354=CARTESIAN_POINT('Origin',(0.,0.,0.));
#5355=CARTESIAN_POINT('Origin',(0.,0.,0.));
#5356=CARTESIAN_POINT('Origin',(0.,0.,0.));
#5357=CARTESIAN_POINT('Origin',(0.,0.,0.));
#5358=CARTESIAN_POINT('Ctrl Pts',(-4.17500251181215,-2.20836332945491,-3.46925408785825));
#5359=CARTESIAN_POINT('Ctrl Pts',(-4.14040488867328,-2.22833827648746,-3.68688706832704));
#5360=CARTESIAN_POINT('Ctrl Pts',(-4.23588660588939,-2.41731472804854,-3.75116187409402));
#5361=CARTESIAN_POINT('Ctrl Pts',(-3.47237194058605,-2.61402727889316,-3.32032231920216));
#5362=CARTESIAN_POINT('Ctrl Pts',(-3.4530385704595,-2.62518940534045,-3.53526375354527));
#5363=CARTESIAN_POINT('Ctrl Pts',(-3.54002001573559,-2.8106620929241,-3.60214640694581));
#5364=CARTESIAN_POINT('Ctrl Pts',(-2.75619783495007,-3.02751059156874,-3.22314629010981));
#5365=CARTESIAN_POINT('Ctrl Pts',(-2.74282792772311,-3.03522971110519,-3.4332526945506));
#5366=CARTESIAN_POINT('Ctrl Pts',(-2.8368931367585,-3.20894943574587,-3.50505407716489));
#5367=CARTESIAN_POINT('Ctrl Pts',(-1.27425813156503,-3.88310887824089,-3.22059942984405));
#5368=CARTESIAN_POINT('Ctrl Pts',(-1.28723743436171,-3.8756152742774,-3.43061871662682));
#5369=CARTESIAN_POINT('Ctrl Pts',(-1.39023091438237,-4.04398746048867,-3.50250721526052));
#5370=CARTESIAN_POINT('Ctrl Pts',(-0.544931331064667,-4.30418590283698,
-3.31662087526347));
#5371=CARTESIAN_POINT('Ctrl Pts',(-0.563680077012917,-4.29336130931743,
-3.53154229295521));
#5372=CARTESIAN_POINT('Ctrl Pts',(-0.68105971431977,-4.46107577825961,-3.59844171492072));
#5373=CARTESIAN_POINT('Ctrl Pts',(0.175648173966054,-4.720212674039,-3.46939095956407));
#5374=CARTESIAN_POINT('Ctrl Pts',(0.141042297810615,-4.70023296212511,-3.68702768697363));
#5375=CARTESIAN_POINT('Ctrl Pts',(0.0251197378185065,-4.87741561294743,
-3.75129874579984));
#5376=CARTESIAN_POINT('Ctrl Pts',(-4.21114049304847,-2.43130309725362,-3.7458852558811));
#5377=CARTESIAN_POINT('Ctrl Pts',(-4.18988746455481,-2.41903264520882,-3.73695337648562));
#5378=CARTESIAN_POINT('Ctrl Pts',(-4.16932200861515,-2.40716260740472,-3.72569031308385));
#5379=CARTESIAN_POINT('Ctrl Pts',(-4.14987580443041,-2.39594091351642,-3.71225681513601));
#5380=CARTESIAN_POINT('Ctrl Pts',(-4.13336582704669,-2.38641360882791,-3.7008516717365));
#5381=CARTESIAN_POINT('Ctrl Pts',(-4.11766043275974,-2.3773497008117,-3.68788163057286));
#5382=CARTESIAN_POINT('Ctrl Pts',(-4.10302583783635,-2.3688968958051,-3.67343984369392));
#5383=CARTESIAN_POINT('Ctrl Pts',(-4.08994531422733,-2.36134170783918,-3.66053165353114));
#5384=CARTESIAN_POINT('Ctrl Pts',(-4.07771995662713,-2.35427354186951,-3.64644578533102));
#5385=CARTESIAN_POINT('Ctrl Pts',(-4.0665555419278,-2.34782521054507,-3.6312629502672));
#5386=CARTESIAN_POINT('Ctrl Pts',(-4.06543294642031,-2.34717682296985,-3.62973629769359));
#5387=CARTESIAN_POINT('Ctrl Pts',(-4.0643210925777,-2.34653473372248,-3.62819858242172));
#5388=CARTESIAN_POINT('Ctrl Pts',(-4.06322019950523,-2.34589909973338,-3.62664990860538));
#5389=CARTESIAN_POINT('Ctrl Pts',(-4.05342647660366,-2.34024439691828,-3.61287265575376));
#5390=CARTESIAN_POINT('Ctrl Pts',(-4.04454702329777,-2.3351426055361,-3.59831218398053));
#5391=CARTESIAN_POINT('Ctrl Pts',(-4.03673870576888,-2.33065236670391,-3.58305397058372));
#5392=CARTESIAN_POINT('Ctrl Pts',(-4.02952082819937,-2.32650166534877,-3.56894953440778));
#5393=CARTESIAN_POINT('Ctrl Pts',(-4.02321878492448,-2.32287395117742,-3.55424736097336));
#5394=CARTESIAN_POINT('Ctrl Pts',(-4.01796736010047,-2.31984083523265,-3.53904370693992));
#5395=CARTESIAN_POINT('Ctrl Pts',(-4.01301173760937,-2.31697856868638,-3.52469644454925));
#5396=CARTESIAN_POINT('Ctrl Pts',(-4.00899243519024,-2.31464674979346,-3.50990175781935));
#5397=CARTESIAN_POINT('Ctrl Pts',(-4.00602358012327,-2.31291900655892,-3.49478367972883));
#5398=CARTESIAN_POINT('Ctrl Pts',(-4.00322852109713,-2.31129240498571,-3.480550610188));
#5399=CARTESIAN_POINT('Ctrl Pts',(-4.00136519487194,-2.31020233875389,-3.46603085078074));
#5400=CARTESIAN_POINT('Ctrl Pts',(-4.00051969176615,-2.30970772649789,-3.45137325050413));
#5401=CARTESIAN_POINT('Ctrl Pts',(-4.00017366263073,-2.3095053023434,-3.44537450642346));
#5402=CARTESIAN_POINT('Ctrl Pts',(-3.99999794474645,-2.30940248824816,-3.43935322510961));
#5403=CARTESIAN_POINT('Ctrl Pts',(-3.99999756070101,-2.30940248527412,-3.43332188518958));
#5404=CARTESIAN_POINT('Ctrl Pts',(2.43945024266171E-6,-4.61880074529696,
-3.4333221894343));
#5405=CARTESIAN_POINT('Ctrl Pts',(1.97908393093112E-6,-4.61880157394924,
-3.44798265290114));
#5406=CARTESIAN_POINT('Ctrl Pts',(1.01218396963414E-5,-4.62000512030333,
-3.4625805024101));
#5407=CARTESIAN_POINT('Ctrl Pts',(2.08731294980132E-5,-4.62231794296185,
-3.47695007304928));
#5408=CARTESIAN_POINT('Ctrl Pts',(3.2443490399229E-5,-4.62480696459119,
-3.49241436815785));
#5409=CARTESIAN_POINT('Ctrl Pts',(4.62192455342729E-5,-4.62857938934421,
-3.50761388627125));
#5410=CARTESIAN_POINT('Ctrl Pts',(5.292240897191E-5,-4.63349822781682,-3.52240062737015));
#5411=CARTESIAN_POINT('Ctrl Pts',(5.99895780237729E-5,-4.63868417671216,
-3.53799034109924));
#5412=CARTESIAN_POINT('Ctrl Pts',(5.84997758187179E-5,-4.64514293602618,
-3.55312199412916));
#5413=CARTESIAN_POINT('Ctrl Pts',(4.82387339152211E-5,-4.65271536558076,
-3.56768197579321));
#5414=CARTESIAN_POINT('Ctrl Pts',(3.67781382146205E-5,-4.66117304019241,
-3.58394407323217));
#5415=CARTESIAN_POINT('Ctrl Pts',(1.388586822648E-5,-4.67101852024403,-3.5994946447632));
#5416=CARTESIAN_POINT('Ctrl Pts',(3.07627714035774E-6,-4.6820576544963,
-3.61422980570673));
#5417=CARTESIAN_POINT('Ctrl Pts',(-1.12741608040529E-8,-4.68521077037762,
-3.6184386203586));
#5418=CARTESIAN_POINT('Ctrl Pts',(-1.95993311524184E-6,-4.68846149517478,
-3.62258112015053));
#5419=CARTESIAN_POINT('Ctrl Pts',(-1.88456980714909E-6,-4.6918058410115,
-3.62665524106977));
#5420=CARTESIAN_POINT('Ctrl Pts',(-1.59706231056096E-6,-4.70456436400585,
-3.64219782188156));
#5421=CARTESIAN_POINT('Ctrl Pts',(7.08251721277811E-6,-4.71861608899416,
-3.65664956360104));
#5422=CARTESIAN_POINT('Ctrl Pts',(1.08520660015016E-5,-4.73369614799714,
-3.66990623170299));
#5423=CARTESIAN_POINT('Ctrl Pts',(1.59548811295723E-5,-4.75410993158917,
-3.68785170219029));
#5424=CARTESIAN_POINT('Ctrl Pts',(1.26337967333387E-5,-4.77640804570073,
-3.70360921007672));
#5425=CARTESIAN_POINT('Ctrl Pts',(7.67272428404579E-6,-4.79999197504746,
-3.71699112236792));
#5426=CARTESIAN_POINT('Ctrl Pts',(3.4527694589582E-6,-4.8200527819513,-3.72837395660776));
#5427=CARTESIAN_POINT('Ctrl Pts',(-7.85645361820395E-9,-4.8410474613116,
-3.73803875904214));
#5428=CARTESIAN_POINT('Ctrl Pts',(-2.82044192924637E-12,-4.86260619451213,
-3.74588525588111));
#5429=CARTESIAN_POINT('Ctrl Pts',(-0.175002511812154,-4.71983990082064,
-3.46925408785825));
#5430=CARTESIAN_POINT('Ctrl Pts',(-0.14040488867328,-4.69986495378808,-3.68688706832704));
#5431=CARTESIAN_POINT('Ctrl Pts',(-0.0244873395123925,-4.87704277227474,
-3.75116187409403));
#5432=CARTESIAN_POINT('Ctrl Pts',(0.527628059414741,-4.31417595138192,-3.32032231920166));
#5433=CARTESIAN_POINT('Ctrl Pts',(0.546961429541539,-4.30301382493536,-3.53526375354356));
#5434=CARTESIAN_POINT('Ctrl Pts',(0.664094766059535,-4.47107830999418,-3.60214640694571));
#5435=CARTESIAN_POINT('Ctrl Pts',(1.24380216504877,-3.90069263870748,-3.22314629010981));
#5436=CARTESIAN_POINT('Ctrl Pts',(1.25717207227527,-3.89297351917098,-3.43325269455078));
#5437=CARTESIAN_POINT('Ctrl Pts',(1.36058516243511,-4.06129624212832,-3.50505407716491));
#5438=CARTESIAN_POINT('Ctrl Pts',(2.72574186843613,-3.04509435203399,-3.22059942984405));
#5439=CARTESIAN_POINT('Ctrl Pts',(2.71276256563965,-3.05258795599766,-3.43061871662663));
#5440=CARTESIAN_POINT('Ctrl Pts',(2.80708041617899,-3.22596901922515,-3.50250721526051));
#5441=CARTESIAN_POINT('Ctrl Pts',(3.45506866893442,-2.62401732743909,-3.31662087526373));
#5442=CARTESIAN_POINT('Ctrl Pts',(3.43631992298652,-2.63484192095947,-3.53154229295476));
#5443=CARTESIAN_POINT('Ctrl Pts',(3.52287509501949,-2.82035290322563,-3.59844171492057));
#5444=CARTESIAN_POINT('Ctrl Pts',(4.17564817396606,-2.20799055623655,-3.46939095956407));
#5445=CARTESIAN_POINT('Ctrl Pts',(4.14104229781062,-2.22797026815043,-3.68702768697362));
#5446=CARTESIAN_POINT('Ctrl Pts',(4.23652569453656,-2.41695347538648,-3.75129874579984));
#5447=CARTESIAN_POINT('Ctrl Pts',(4.00000000017051,-2.30939825748223,-3.43332219633194));
#5448=CARTESIAN_POINT('Ctrl Pts',(4.00000048725084,-2.30939907077008,-3.44798266367369));
#5449=CARTESIAN_POINT('Ctrl Pts',(4.00104686059629,-2.30999379289612,-3.46258051754916));
#5450=CARTESIAN_POINT('Ctrl Pts',(4.00305520041485,-2.31114089450209,-3.47695009281808));
#5451=CARTESIAN_POINT('Ctrl Pts',(4.00521654264325,-2.31237538635369,-3.49241439300576));
#5452=CARTESIAN_POINT('Ctrl Pts',(4.00849044815729,-2.31424967029535,-3.50761391649764));
#5453=CARTESIAN_POINT('Ctrl Pts',(4.01275364170441,-2.3167032865241,-3.52240066296025));
#5454=CARTESIAN_POINT('Ctrl Pts',(4.01724834205715,-2.31929014297502,-3.53799038315636));
#5455=CARTESIAN_POINT('Ctrl Pts',(4.02284105122292,-2.3225208156867,-3.55312204258641));
#5456=CARTESIAN_POINT('Ctrl Pts',(4.02939384253155,-2.32631592007399,-3.56768203020858));
#5457=CARTESIAN_POINT('Ctrl Pts',(4.0367126808535,-2.33055468705393,-3.58394413750869));
#5458=CARTESIAN_POINT('Ctrl Pts',(4.04522767987659,-2.33549725770526,-3.59949471806542));
#5459=CARTESIAN_POINT('Ctrl Pts',(4.05478245648888,-2.34102619219696,-3.6142298866834));
#5460=CARTESIAN_POINT('Ctrl Pts',(4.05751157529791,-2.34260541479184,-3.61843867433604));
#5461=CARTESIAN_POINT('Ctrl Pts',(4.06032579428629,-2.3442324549239,-3.62258114793907));
#5462=CARTESIAN_POINT('Ctrl Pts',(4.06322210246804,-2.34590455216165,-3.6266552435119));
#5463=CARTESIAN_POINT('Ctrl Pts',(4.07427144977102,-2.35228356362894,-3.64219782189265));
#5464=CARTESIAN_POINT('Ctrl Pts',(4.08644493860459,-2.35930190796122,-3.65664956136288));
#5465=CARTESIAN_POINT('Ctrl Pts',(4.09950653555256,-2.36683867144495,-3.66990622752824));
#5466=CARTESIAN_POINT('Ctrl Pts',(4.11718794719008,-2.37704114654056,-3.6878517032878));
#5467=CARTESIAN_POINT('Ctrl Pts',(4.13649702594183,-2.38819308295317,-3.70360921509657));
#5468=CARTESIAN_POINT('Ctrl Pts',(4.15691883376619,-2.39998934777108,-3.71699112998034));
#5469=CARTESIAN_POINT('Ctrl Pts',(4.17428988954401,-2.41002340429949,-3.72837396111162));
#5470=CARTESIAN_POINT('Ctrl Pts',(4.19247008180213,-2.42052373938338,-3.73803876108225));
#5471=CARTESIAN_POINT('Ctrl Pts',(4.21114049294513,-2.43130309720049,-3.74588525620001));
#5472=CARTESIAN_POINT('Ctrl Pts',(-4.,2.51147855358203,-3.46925445172476));
#5473=CARTESIAN_POINT('Ctrl Pts',(-4.,2.47152863417759,-3.68688744215519));
#5474=CARTESIAN_POINT('Ctrl Pts',(-4.21139928416427,2.45972999598821,-3.75116223796054));
#5475=CARTESIAN_POINT('Ctrl Pts',(-4.,1.70009491919674,-3.32031236430177));
#5476=CARTESIAN_POINT('Ctrl Pts',(-4.,1.67777237333276,-3.53525372389719));
#5477=CARTESIAN_POINT('Ctrl Pts',(-4.20411429709547,1.66036317409662,-3.60213643185789));
#5478=CARTESIAN_POINT('Ctrl Pts',(-4.,0.873073999173834,-3.22313462962843));
#5479=CARTESIAN_POINT('Ctrl Pts',(-4.,0.857636899345751,-3.4332406327822));
#5480=CARTESIAN_POINT('Ctrl Pts',(-4.19747753477223,0.852241327372437,-3.50504241668323));
#5481=CARTESIAN_POINT('Ctrl Pts',(-4.,-0.838224073004193,-3.22061061976714));
#5482=CARTESIAN_POINT('Ctrl Pts',(-4.,-0.823233910613052,-3.43063028686274));
#5483=CARTESIAN_POINT('Ctrl Pts',(-4.19731206413347,-0.818222978799002,
-3.50251840518389));
#5484=CARTESIAN_POINT('Ctrl Pts',(-4.,-1.68011768235794,-3.31661159321879));
#5485=CARTESIAN_POINT('Ctrl Pts',(-3.99999999999891,-1.65846997463859,-3.53153291307526));
#5486=CARTESIAN_POINT('Ctrl Pts',(-4.20393436246917,-1.64067374345485,-3.59843261460693));
#5487=CARTESIAN_POINT('Ctrl Pts',(-4.,-2.51222074532931,-3.46939070756972));
#5488=CARTESIAN_POINT('Ctrl Pts',(-4.,-2.47226133904334,-3.68702742808119));
#5489=CARTESIAN_POINT('Ctrl Pts',(-4.2114059444014,-2.46046078616939,-3.75129849380549));
#5490=CARTESIAN_POINT('Ctrl Pts',(-4.21114049294319,2.43130309719935,-3.74588525620613));
#5491=CARTESIAN_POINT('Ctrl Pts',(-4.18988744800146,2.41903265632003,-3.73695337399635));
#5492=CARTESIAN_POINT('Ctrl Pts',(-4.16932495849824,2.40715746377534,-3.72569030631416));
#5493=CARTESIAN_POINT('Ctrl Pts',(-4.14988357794915,2.39592740031508,-3.71225680267033));
#5494=CARTESIAN_POINT('Ctrl Pts',(-4.13337770500439,2.38639299507217,-3.70085166074699));
#5495=CARTESIAN_POINT('Ctrl Pts',(-4.11767543656294,2.37732368080158,-3.68788162176546));
#5496=CARTESIAN_POINT('Ctrl Pts',(-4.10303779813105,2.36887615430201,-3.67343983757684));
#5497=CARTESIAN_POINT('Ctrl Pts',(-4.08995455343392,2.36132568386283,-3.66053164905436));
#5498=CARTESIAN_POINT('Ctrl Pts',(-4.07772066494259,2.35427229783089,-3.64644578275999));
#5499=CARTESIAN_POINT('Ctrl Pts',(-4.06655404023516,2.34782779780516,-3.63126294971765));
#5500=CARTESIAN_POINT('Ctrl Pts',(-4.06543122325348,2.34717979590156,-3.62973629836));
#5501=CARTESIAN_POINT('Ctrl Pts',(-4.06431923159962,2.3465379473787,-3.62819858431993));
#5502=CARTESIAN_POINT('Ctrl Pts',(-4.06321831073147,2.34590236352179,-3.62664991175086));
#5503=CARTESIAN_POINT('Ctrl Pts',(-4.05342432406475,2.3402480971705,-3.61287264679811));
#5504=CARTESIAN_POINT('Ctrl Pts',(-4.0445663092799,2.33510915669676,-3.59831216137955));
#5505=CARTESIAN_POINT('Ctrl Pts',(-4.03677348473163,2.33059207189997,-3.58305393336723));
#5506=CARTESIAN_POINT('Ctrl Pts',(-4.0295699301827,2.32641655549583,-3.56894948675407));
#5507=CARTESIAN_POINT('Ctrl Pts',(-4.0232772145443,2.3227726820216,-3.55424730231654));
#5508=CARTESIAN_POINT('Ctrl Pts',(-4.0180247471138,2.31974137256816,-3.53904363726008));
#5509=CARTESIAN_POINT('Ctrl Pts',(-4.01306814118424,2.31688081101113,-3.52469636574108));
#5510=CARTESIAN_POINT('Ctrl Pts',(-4.00903907788616,2.31456590326902,-3.5099016699489));
#5511=CARTESIAN_POINT('Ctrl Pts',(-4.0060583845751,2.31285867251372,-3.49478358336693));
#5512=CARTESIAN_POINT('Ctrl Pts',(-4.00325218017958,2.31125138254802,-3.48055050515637));
#5513=CARTESIAN_POINT('Ctrl Pts',(-4.0013764967891,2.31018272987839,-3.466030737562));
#5514=CARTESIAN_POINT('Ctrl Pts',(-4.00052540443089,2.30969781163208,-3.45137313002631));
#5515=CARTESIAN_POINT('Ctrl Pts',(-4.00017709632775,2.30949935966277,-3.44537452901903));
#5516=CARTESIAN_POINT('Ctrl Pts',(-4.00000020054081,2.3093985918993,-3.43935339203637));
#5517=CARTESIAN_POINT('Ctrl Pts',(-4.00000000017049,2.30939825730392,-3.43332219680665));
#5518=CARTESIAN_POINT('Ctrl Pts',(4.,-2.51147557650728,-3.46925390523664));
#5519=CARTESIAN_POINT('Ctrl Pts',(4.,-2.47152569515979,-3.68688688070577));
#5520=CARTESIAN_POINT('Ctrl Pts',(4.21139925744971,-2.45972706465252,-3.75116169147242));
#5521=CARTESIAN_POINT('Ctrl Pts',(4.,-1.70017543050729,-3.32032727503766));
#5522=CARTESIAN_POINT('Ctrl Pts',(4.,-1.6778503894312,-3.53526875834698));
#5523=CARTESIAN_POINT('Ctrl Pts',(4.20411502351679,-1.6604426695002,-3.60215138177456));
#5524=CARTESIAN_POINT('Ctrl Pts',(4.,-0.873247063144998,-3.22315549424076));
#5525=CARTESIAN_POINT('Ctrl Pts',(4.,-0.857808282953852,-3.43326221544981));
#5526=CARTESIAN_POINT('Ctrl Pts',(4.19747890258699,-0.852410278374835,-3.5050632812955));
#5527=CARTESIAN_POINT('Ctrl Pts',(4.,0.837828026423296,-3.22059060139564));
#5528=CARTESIAN_POINT('Ctrl Pts',(4.,0.822843528041621,-3.43060958814149));
#5529=CARTESIAN_POINT('Ctrl Pts',(4.19731075179729,0.817836398951625,-3.50249838681244));
#5530=CARTESIAN_POINT('Ctrl Pts',(4.,1.68022822914713,-3.31663178303255));
#5531=CARTESIAN_POINT('Ctrl Pts',(4.00000000000109,1.65857727852441,-3.53155330955454));
#5532=CARTESIAN_POINT('Ctrl Pts',(4.20393533543406,1.64078067129417,-3.5984524478792));
#5533=CARTESIAN_POINT('Ctrl Pts',(4.,2.51222311093255,-3.4693911419088));
#5534=CARTESIAN_POINT('Ctrl Pts',(4.,2.47226367441142,-3.68702787430986));
#5535=CARTESIAN_POINT('Ctrl Pts',(4.21140596563046,2.46046311543628,-3.75129892814458));
#5536=CARTESIAN_POINT('Ctrl Pts',(3.99999756073998,2.30940248527475,-3.4333224880889));
#5537=CARTESIAN_POINT('Ctrl Pts',(3.99999852262203,2.3094025091568,-3.44798295458757));
#5538=CARTESIAN_POINT('Ctrl Pts',(4.00103676710518,2.31001134244407,-3.46258080581231));
#5539=CARTESIAN_POINT('Ctrl Pts',(4.00303436866837,2.31117707280252,-3.47695037704058));
#5540=CARTESIAN_POINT('Ctrl Pts',(4.00518415465818,2.31243161266605,-3.4924146735626));
#5541=CARTESIAN_POINT('Ctrl Pts',(4.00844429763966,2.31432976392346,-3.50761419176313));
#5542=CARTESIAN_POINT('Ctrl Pts',(4.01270080012744,2.31679499682455,-3.5224009318679));
#5543=CARTESIAN_POINT('Ctrl Pts',(4.01718844624318,2.3193941008741,-3.53799064595499));
#5544=CARTESIAN_POINT('Ctrl Pts',(4.0227826569856,2.32262219950312,-3.55312229806423));
#5545=CARTESIAN_POINT('Ctrl Pts',(4.02934571990586,2.32639953709204,-3.56768227773151));
#5546=CARTESIAN_POINT('Ctrl Pts',(4.03667602891417,2.330618459277,-3.58394437233773));
#5547=CARTESIAN_POINT('Ctrl Pts',(4.04521392823684,2.33552138396257,-3.5994949397553));
#5548=CARTESIAN_POINT('Ctrl Pts',(4.05477952071165,2.34103159972093,-3.61423009542096));
#5549=CARTESIAN_POINT('Ctrl Pts',(4.0575116841041,2.3426054499366,-3.61843881045851));
#5550=CARTESIAN_POINT('Ctrl Pts',(4.0603278059077,2.34422908860512,-3.6225812136314));
#5551=CARTESIAN_POINT('Ctrl Pts',(4.06322399022508,2.34590128842043,-3.62665524106974));
#5552=CARTESIAN_POINT('Ctrl Pts',(4.07427305149928,2.35228079890645,-3.64219782188164));
#5553=CARTESIAN_POINT('Ctrl Pts',(4.08643786251645,2.35931417813704,-3.65664956360123));
#5554=CARTESIAN_POINT('Ctrl Pts',(4.09949569192928,2.36685747216364,-3.66990623170327));
#5555=CARTESIAN_POINT('Ctrl Pts',(4.11717199569582,2.37706878312497,-3.68785170218656));
#5556=CARTESIAN_POINT('Ctrl Pts',(4.13648438951043,2.38821496403467,-3.70360921006995));
#5557=CARTESIAN_POINT('Ctrl Pts',(4.15691115197695,2.40000263229036,-3.7169911223592));
#5558=CARTESIAN_POINT('Ctrl Pts',(4.17428643035753,2.41002938115652,-3.72837395660282));
#5559=CARTESIAN_POINT('Ctrl Pts',(4.19247008634537,2.42052372384928,-3.73803875904013));
#5560=CARTESIAN_POINT('Ctrl Pts',(4.21114049304847,2.4313030972536,-3.74588525588109));
#5561=CARTESIAN_POINT('Ctrl Pts',(0.175002511812157,4.71983990082062,-3.46925408785825));
#5562=CARTESIAN_POINT('Ctrl Pts',(0.140404888673282,4.69986495378807,-3.68688706832704));
#5563=CARTESIAN_POINT('Ctrl Pts',(0.0244873395123948,4.87704277227473,-3.75116187409402));
#5564=CARTESIAN_POINT('Ctrl Pts',(-0.527628059414645,4.31417595138197,-3.32032231920172));
#5565=CARTESIAN_POINT('Ctrl Pts',(-0.546961429541692,4.30301382493627,-3.53526375354374));
#5566=CARTESIAN_POINT('Ctrl Pts',(-0.664094766059743,4.47107830999488,-3.60214640694596));
#5567=CARTESIAN_POINT('Ctrl Pts',(-1.24380216504891,3.90069263870738,-3.22314629010981));
#5568=CARTESIAN_POINT('Ctrl Pts',(-1.25717207227574,3.8929735191712,-3.43325269455078));
#5569=CARTESIAN_POINT('Ctrl Pts',(-1.36058516243547,4.06129624212829,-3.50505407716496));
#5570=CARTESIAN_POINT('Ctrl Pts',(-2.72574186843599,3.04509435203406,-3.22059942984405));
#5571=CARTESIAN_POINT('Ctrl Pts',(-2.71276256563901,3.05258795599751,-3.43061871662663));
#5572=CARTESIAN_POINT('Ctrl Pts',(-2.80708041617863,3.22596901922515,-3.50250721526044));
#5573=CARTESIAN_POINT('Ctrl Pts',(-3.45506866893449,2.62401732743904,-3.31662087526396));
#5574=CARTESIAN_POINT('Ctrl Pts',(-3.43631992298762,2.63484192096129,-3.53154229295572));
#5575=CARTESIAN_POINT('Ctrl Pts',(-3.52287509501967,2.82035290322543,-3.59844171492059));
#5576=CARTESIAN_POINT('Ctrl Pts',(-4.17564817396606,2.20799055623653,-3.46939095956406));
#5577=CARTESIAN_POINT('Ctrl Pts',(-4.14104229781062,2.22797026815042,-3.68702768697362));
#5578=CARTESIAN_POINT('Ctrl Pts',(-4.23652569453656,2.41695347538647,-3.75129874579984));
#5579=CARTESIAN_POINT('Ctrl Pts',(2.82335279537585E-12,4.86260619451211,
-3.7458852558811));
#5580=CARTESIAN_POINT('Ctrl Pts',(8.94255681535868E-9,4.83806530590424,
-3.73695337648466));
#5581=CARTESIAN_POINT('Ctrl Pts',(-2.9647450864845E-6,4.8143200797156,-3.72569031308144));
#5582=CARTESIAN_POINT('Ctrl Pts',(-7.79485668908126E-6,4.79186832593817,
-3.7122568151317));
#5583=CARTESIAN_POINT('Ctrl Pts',(-1.18956587044119E-5,4.77280661376393,
-3.70085167173177));
#5584=CARTESIAN_POINT('Ctrl Pts',(-1.50182025258554E-5,4.75467338932713,
-3.68788163056771));
#5585=CARTESIAN_POINT('Ctrl Pts',(-1.19717952318522E-5,4.73777305584639,
-3.67343984368836));
#5586=CARTESIAN_POINT('Ctrl Pts',(-9.24889085760412E-6,4.72266739612336,
-3.6605316535251));
#5587=CARTESIAN_POINT('Ctrl Pts',(-7.16403024165593E-7,4.70854584288659,
-3.64644578532448));
#5588=CARTESIAN_POINT('Ctrl Pts',(1.49498629956454E-6,4.69565301047662,
-3.63126295026017));
#5589=CARTESIAN_POINT('Ctrl Pts',(1.71734419142002E-6,4.69435662046335,
-3.62973629768884));
#5590=CARTESIAN_POINT('Ctrl Pts',(1.85602259680142E-6,4.69307268216863,
-3.62819858241928));
#5591=CARTESIAN_POINT('Ctrl Pts',(1.88466842695255E-6,4.69180146380839,
-3.62664990860529));
#5592=CARTESIAN_POINT('Ctrl Pts',(2.13950640372796E-6,4.680492497957,-3.61287265378804));
#5593=CARTESIAN_POINT('Ctrl Pts',(-1.9306210438466E-5,4.67025176882188,
-3.59831217982513));
#5594=CARTESIAN_POINT('Ctrl Pts',(-3.48040781505873E-5,4.66124444713254,
-3.58305396405286));
#5595=CARTESIAN_POINT('Ctrl Pts',(-4.91300462124437E-5,4.652918230569,-3.56894952621052));
#5596=CARTESIAN_POINT('Ctrl Pts',(-5.84590505708E-5,4.64564664360582,-3.55424735099498));
#5597=CARTESIAN_POINT('Ctrl Pts',(-5.74159969723896E-5,4.63958221831933,
-3.53904369510472));
#5598=CARTESIAN_POINT('Ctrl Pts',(-5.64316965346851E-5,4.63385939019907,
-3.52469643129172));
#5599=CARTESIAN_POINT('Ctrl Pts',(-4.66685024715262E-5,4.62921266308804,
-3.50990174309249));
#5600=CARTESIAN_POINT('Ctrl Pts',(-3.48265015805382E-5,4.62577768814575,
-3.49478366353225));
#5601=CARTESIAN_POINT('Ctrl Pts',(-2.3677727972645E-5,4.62254379563611,
-3.48055059194621));
#5602=CARTESIAN_POINT('Ctrl Pts',(-1.13157927300613E-5,4.6203850753921,
-3.46603083046657));
#5603=CARTESIAN_POINT('Ctrl Pts',(-5.72057276286163E-6,4.61940554316572,
-3.45137322816867));
#5604=CARTESIAN_POINT('Ctrl Pts',(-3.43072437850262E-6,4.61900466879454,
-3.4453745923443));
#5605=CARTESIAN_POINT('Ctrl Pts',(-2.25005174120207E-6,4.61880108620347,
-3.43935342011916));
#5606=CARTESIAN_POINT('Ctrl Pts',(-2.4394502271739E-6,4.61880074529695,
-3.43332218943429));
#5607=CARTESIAN_POINT('Ctrl Pts',(4.17500251181215,2.20836332945489,-3.46925408785824));
#5608=CARTESIAN_POINT('Ctrl Pts',(4.14040488867328,2.22833827648744,-3.68688706832703));
#5609=CARTESIAN_POINT('Ctrl Pts',(4.23588660588939,2.41731472804853,-3.75116187409402));
#5610=CARTESIAN_POINT('Ctrl Pts',(3.47237194058599,2.61402727889318,-3.32032231920177));
#5611=CARTESIAN_POINT('Ctrl Pts',(3.45303857046027,2.62518940534083,-3.53526375354359));
#5612=CARTESIAN_POINT('Ctrl Pts',(3.5400200157356,2.81066209292438,-3.60214640694587));
#5613=CARTESIAN_POINT('Ctrl Pts',(2.75619783495023,3.02751059156863,-3.22314629010981));
#5614=CARTESIAN_POINT('Ctrl Pts',(2.74282792772345,3.03522971110461,-3.43325269455059));
#5615=CARTESIAN_POINT('Ctrl Pts',(2.83689313675868,3.20894943574584,-3.50505407716491));
#5616=CARTESIAN_POINT('Ctrl Pts',(1.27425813156487,3.88310887824096,-3.22059942984405));
#5617=CARTESIAN_POINT('Ctrl Pts',(1.28723743436204,3.87561527427756,-3.43061871662681));
#5618=CARTESIAN_POINT('Ctrl Pts',(1.39023091438219,4.04398746048866,-3.50250721526049));
#5619=CARTESIAN_POINT('Ctrl Pts',(0.544931331064781,4.3041859028369,-3.31662087526338));
#5620=CARTESIAN_POINT('Ctrl Pts',(0.563680077013038,4.29336130931717,-3.5315422929541));
#5621=CARTESIAN_POINT('Ctrl Pts',(0.681059714319705,4.46107577825929,-3.5984417149206));
#5622=CARTESIAN_POINT('Ctrl Pts',(-0.175648173966052,4.72021267403898,-3.46939095956407));
#5623=CARTESIAN_POINT('Ctrl Pts',(-0.141042297810612,4.70023296212509,-3.68702768697363));
#5624=CARTESIAN_POINT('Ctrl Pts',(-0.0251197378185046,4.87741561294741,
-3.75129874579984));
#5679=UNCERTAINTY_MEASURE_WITH_UNIT(LENGTH_MEASURE(0.01),#5690,
'DISTANCE_ACCURACY_VALUE',
'Maximum model space distance between geometric entities at asserted c
onnectivities');
#5680=UNCERTAINTY_MEASURE_WITH_UNIT(LENGTH_MEASURE(0.01),#5690,
'DISTANCE_ACCURACY_VALUE',
'Maximum model space distance between geometric entities at asserted c
onnectivities');
#5688=(
GEOMETRIC_REPRESENTATION_CONTEXT(3)
GLOBAL_UNCERTAINTY_ASSIGNED_CONTEXT((#5679))
GLOBAL_UNIT_ASSIGNED_CONTEXT((#5690,#5692,#5693))
REPRESENTATION_CONTEXT('','3D')
);
#5689=(
GEOMETRIC_REPRESENTATION_CONTEXT(3)
GLOBAL_UNCERTAINTY_ASSIGNED_CONTEXT((#5680))
GLOBAL_UNIT_ASSIGNED_CONTEXT((#5690,#5692,#5693))
REPRESENTATION_CONTEXT('','3D')
);
#5690=(
LENGTH_UNIT()
NAMED_UNIT(*)
SI_UNIT(.MILLI.,.METRE.)
);
#5692=(
NAMED_UNIT(*)
PLANE_ANGLE_UNIT()
SI_UNIT($,.RADIAN.)
);
#5693=(
NAMED_UNIT(*)
SI_UNIT($,.STERADIAN.)
SOLID_ANGLE_UNIT()
);
#5701=SHAPE_DEFINITION_REPRESENTATION(#5709,#5764);
#5709=PRODUCT_DEFINITION_SHAPE('',$,#5773);
#5764=SHAPE_REPRESENTATION('',(#3284),#5688);
#5765=PRODUCT_DEFINITION_CONTEXT('part definition',#5791,'design');
#5773=PRODUCT_DEFINITION(
'hex flange nut gradea_iso_ISO - 4161 - M5 - N',
'hex flange nut gradea_iso_ISO - 4161 - M5 - N',#5781,#5765);
#5781=PRODUCT_DEFINITION_FORMATION('',$,#5800);
#5791=APPLICATION_CONTEXT(
'Core Data for Automotive Mechanical Design Process');
#5792=PRODUCT_CONTEXT('part definition',#5791,'mechanical');
#5800=PRODUCT('hex flange nut gradea_iso_ISO - 4161 - M5 - N',
'hex flange nut gradea_iso_ISO - 4161 - M5 - N',$,(#5792));
#5806=PRESENTATION_STYLE_ASSIGNMENT((#5812));
#5812=SURFACE_STYLE_USAGE(.BOTH.,#5818);
#5818=SURFACE_SIDE_STYLE('',(#5824));
#5824=SURFACE_STYLE_FILL_AREA(#5830);
#5830=FILL_AREA_STYLE('Opaque(31,36,43)',(#5836));
#5836=FILL_AREA_STYLE_COLOUR('Opaque(31,36,43)',#5842);
#5842=COLOUR_RGB('Opaque(31,36,43)',0.12156862745098,0.141176470588235,
0.168627450980392);
ENDSEC;
END-ISO-10303-21;
